ISO-10303-21;
HEADER;
FILE_DESCRIPTION (('STEP AP214'),
    '1' );
FILE_NAME ('hex flange nut gradea_iso_ISO - 4161 - M5 - N.step',
    '2026-10-31T03:46:07',
    ( '' ),
    ( '' ),
    'SwSTEP 2.0',
    'SolidWorks 2026',
    '' );
FILE_SCHEMA (( 'AUTOMOTIVE_DESIGN' ));
ENDSEC;

DATA;
#10=CARTESIAN_POINT ( 'NONE',  ( 4.000000000000000000, 2.309401076758515803, -0.4999999999999995559 ) ) ;
#12=VERTEX_POINT ( 'NONE', #4836 ) ;
#57=CARTESIAN_POINT ( 'NONE',  ( 3.511755186886750923, -2.826662030176382956, -3.597382984111582083 ) ) ;
#61=CARTESIAN_POINT ( 'NONE',  ( -4.204015924366189871, 1.626724848190922446, -3.610627190413390419 ) ) ;
#76=CARTESIAN_POINT ( 'NONE',  ( 3.333333333333335702, -2.694301256218268215, -3.300726591567084256 ) ) ;
#91=CARTESIAN_POINT ( 'NONE',  ( -2.688821387764050996E-14, -4.618802153517012954, -0.4999999999999995559 ) ) ;
#94=PLANE ( 'NONE',  #21616 ) ;
#126=ORIENTED_EDGE ( 'NONE', *, *, #10672, .T. ) ;
#160=VERTEX_POINT ( 'NONE', #20384 ) ;
#205=CARTESIAN_POINT ( 'NONE',  ( 2.500000000000000444, 0.000000000000000000, -25.03750572909317285 ) ) ;
#222=CARTESIAN_POINT ( 'NONE',  ( -6.259644161404862988E-16, -4.618802153517027165, -3.504271511726793076 ) ) ;
#226=PRODUCT_CONTEXT ( 'NONE', #16017, 'mechanical' ) ;
#234=AXIS2_PLACEMENT_3D ( 'NONE', #5498, #20216, #1399 ) ;
#251=CARTESIAN_POINT ( 'NONE',  ( 2.171643655288379993, -3.365003104552334978, -1.195831703456429434E-14 ) ) ;
#262=ORIENTED_EDGE ( 'NONE', *, *, #21312, .T. ) ;
#287=B_SPLINE_CURVE_WITH_KNOTS ( 'NONE', 3,
 ( #4125, #526, #13356, #5838, #13245, #20670, #11305, #18611 ),
 .UNSPECIFIED., .F., .F.,
 ( 4, 2, 2, 4 ),
 ( 0.000000000000000000, 0.002450665683189820997, 0.003675998524784731495, 0.004901331366379641993 ),
 .UNSPECIFIED. ) ;
#293=DIRECTION ( 'NONE',  ( 0.000000000000000000, 0.000000000000000000, -1.000000000000000000 ) ) ;
#316=CARTESIAN_POINT ( 'NONE',  ( 4.211140560182196957, 2.431303136016536470, -3.745885042887433514 ) ) ;
#345=SHAPE_DEFINITION_REPRESENTATION ( #14626, #5587 ) ;
#379=CARTESIAN_POINT ( 'NONE',  ( 2.742827927723449299, 3.035229711104609596, -3.433252694550591233 ) ) ;
#388=ORIENTED_EDGE ( 'NONE', *, *, #7363, .F. ) ;
#389=DIRECTION ( 'NONE',  ( 0.000000000000000000, 0.000000000000000000, -1.000000000000000000 ) ) ;
#453=DIRECTION ( 'NONE',  ( 0.000000000000000000, 0.000000000000000000, 1.000000000000000000 ) ) ;
#464=DIRECTION ( 'NONE',  ( 1.000000000000000000, 0.000000000000000000, 0.000000000000000000 ) ) ;
#492=ORIENTED_EDGE ( 'NONE', *, *, #8852, .T. ) ;
#520=( BOUNDED_SURFACE ( )  B_SPLINE_SURFACE ( 3, 2, ( 
 ( #8768, #10596, #14345 ),
 ( #16129, #20203, #12794 ),
 ( #5133, #12544, #19859 ),
 ( #3307, #8898, #16259 ),
 ( #23601, #7057, #14447 ),
 ( #7298, #3652, #21785 ) ),
 .UNSPECIFIED., .F., .F., .F. ) 
 B_SPLINE_SURFACE_WITH_KNOTS ( ( 4, 2, 4 ),
 ( 3, 3 ),
 ( 0.02032853247518125531, 0.02278863295364820865, 0.02524873343211516200 ),
 ( 0.000000000000000000, 1.000000000000000000 ),
 .UNSPECIFIED. ) 
 GEOMETRIC_REPRESENTATION_ITEM ( )  RATIONAL_B_SPLINE_SURFACE ( (
 ( 1.000000000000000000, 0.8047781615896836271, 1.000000000000000000),
 ( 1.000000000000000000, 0.8123767586289967202, 1.000000000000000000),
 ( 1.000000000000000000, 0.8190662415563443322, 1.000000000000000000),
 ( 1.000000000000000000, 0.8192361015669982205, 1.000000000000000000),
 ( 1.000000000000000000, 0.8126135807103181952, 1.000000000000000000),
 ( 1.000000000000000000, 0.8047712338318587788, 1.000000000000000000) ) ) 
 REPRESENTATION_ITEM ( '' )  SURFACE ( )  );
#526=CARTESIAN_POINT ( 'NONE',  ( -3.511755186886750479, 2.826662030176366081, -3.597382984111578086 ) ) ;
#552=ORIENTED_EDGE ( 'NONE', *, *, #1635, .T. ) ;
#556=CARTESIAN_POINT ( 'NONE',  ( 3.679171394226031122, 2.494631558665830973, -0.3503314178412474389 ) ) ;
#561=ORIENTED_EDGE ( 'NONE', *, *, #3975, .T. ) ;
#564=ORIENTED_EDGE ( 'NONE', *, *, #13021, .F. ) ;
#600=CARTESIAN_POINT ( 'NONE',  ( 2.100000000000000089, 0.000000000000000000, -4.694516984716113228 ) ) ;
#608=FACE_OUTER_BOUND ( 'NONE', #10956, .T. ) ;
#611=CIRCLE ( 'NONE', #234, 2.100000000000000089 ) ;
#652=FACE_OUTER_BOUND ( 'NONE', #16462, .T. ) ;
#688=ORIENTED_EDGE ( 'NONE', *, *, #3854, .T. ) ;
#696=DIRECTION ( 'NONE',  ( 1.000000000000000000, 0.000000000000000000, 0.000000000000000000 ) ) ;
#739=ORIENTED_EDGE ( 'NONE', *, *, #5618, .F. ) ;
#757=CARTESIAN_POINT ( 'NONE',  ( 4.197393957002303999, 7.772902908466098641E-14, -3.503767560748929810 ) ) ;
#760=AXIS2_PLACEMENT_3D ( 'NONE', #10210, #12066, #20943 ) ;
#762=CIRCLE ( 'NONE', #20827, 2.499999999999999556 ) ;
#841=CARTESIAN_POINT ( 'NONE',  ( 2.836893136758676270, 3.208949435745843903, -3.505054077164911241 ) ) ;
#890=ORIENTED_EDGE ( 'NONE', *, *, #22306, .T. ) ;
#953=CARTESIAN_POINT ( 'NONE',  ( 0.6640947660595348800, -4.471078309994175548, -3.602146406945708090 ) ) ;
#972=LINE ( 'NONE', #15862, #14857 ) ;
#1017=B_SPLINE_CURVE_WITH_KNOTS ( 'NONE', 3,
 ( #1766, #14723, #19115, #11107, #18876 ),
 .UNSPECIFIED., .F., .F.,
 ( 4, 1, 4 ),
 ( 0.000000000000000000, 0.002309401076758506657, 0.004618802153517013315 ),
 .UNSPECIFIED. ) ;
#1033=CARTESIAN_POINT ( 'NONE',  ( -6.259644161404860030E-16, -4.618802153517027165, -3.433295621305388234 ) ) ;
#1048=CIRCLE ( 'NONE', #19178, 4.000000000000000000 ) ;
#1063=CARTESIAN_POINT ( 'NONE',  ( -2.688821387764050996E-14, -4.618802153517012954, -0.4999999999999995559 ) ) ;
#1072=CARTESIAN_POINT ( 'NONE',  ( 1.243802165048773611, -3.900692638707475624, -3.223146290109810241 ) ) ;
#1076=DIRECTION ( 'NONE',  ( -1.000000000000000000, 0.000000000000000000, 0.000000000000000000 ) ) ;
#1092=ORIENTED_EDGE ( 'NONE', *, *, #7396, .F. ) ;
#1118=TOROIDAL_SURFACE ( 'NONE', #6977, 5.384454397937118664, 0.5155456020628804703 ) ;
#1181=DIRECTION ( 'NONE',  ( -1.000000000000000000, 0.000000000000000000, 0.000000000000000000 ) ) ;
#1204=ORIENTED_EDGE ( 'NONE', *, *, #18714, .T. ) ;
#1253=CARTESIAN_POINT ( 'NONE',  ( -3.472371940586054251, -2.614027278893156669, -3.320322319202162031 ) ) ;
#1261=CARTESIAN_POINT ( 'NONE',  ( 4.211140560182196957, -2.431303136016555122, -3.745885042887436622 ) ) ;
#1281=DIRECTION ( 'NONE',  ( -0.000000000000000000, -0.000000000000000000, 1.000000000000000000 ) ) ;
#1283=CARTESIAN_POINT ( 'NONE',  ( 4.000000000000000000, -1.084202172485504434E-14, -3.142992957459231906 ) ) ;
#1290=DIRECTION ( 'NONE',  ( 0.000000000000000000, 0.000000000000000000, -1.000000000000000000 ) ) ;
#1305=ORIENTED_EDGE ( 'NONE', *, *, #23640, .T. ) ;
#1352=VERTEX_POINT ( 'NONE', #2279 ) ;
#1398=VERTEX_POINT ( 'NONE', #600 ) ;
#1399=DIRECTION ( 'NONE',  ( -1.000000000000000000, 0.000000000000000000, 0.000000000000000000 ) ) ;
#1421=FACE_OUTER_BOUND ( 'NONE', #4724, .T. ) ;
#1470=EDGE_CURVE ( 'NONE', #19949, #13282, #5988, .T. ) ;
#1496=CARTESIAN_POINT ( 'NONE',  ( -4.207491450040567571, 2.029819825146470524, -3.671670828759566074 ) ) ;
#1506=VERTEX_POINT ( 'NONE', #1063 ) ;
#1540=FACE_OUTER_BOUND ( 'NONE', #15740, .T. ) ;
#1543=VECTOR ( 'NONE', #23799, 1000.000000000000114 ) ;
#1547=DIRECTION ( 'NONE',  ( 0.8660254037844379305, 0.5000000000000013323, 0.000000000000000000 ) ) ;
#1613=CARTESIAN_POINT ( 'NONE',  ( 4.203935335434060505, 1.640780671294165272, -3.598452447879202598 ) ) ;
#1631=CARTESIAN_POINT ( 'NONE',  ( -4.000000000000000000, 2.309401076758498483, -3.433295621305379353 ) ) ;
#1635=EDGE_CURVE ( 'NONE', #4882, #20887, #19861, .T. ) ;
#1675=ORIENTED_EDGE ( 'NONE', *, *, #8013, .F. ) ;
#1679=EDGE_CURVE ( 'NONE', #23662, #12107, #2064, .T. ) ;
#1703=LINE ( 'NONE', #16446, #1543 ) ;
#1726=CARTESIAN_POINT ( 'NONE',  ( 0.000000000000000000, 0.000000000000000000, -0.2800830152838844622 ) ) ;
#1732=FACE_BOUND ( 'NONE', #9168, .T. ) ;
#1766=CARTESIAN_POINT ( 'NONE',  ( 1.567478505476134606E-15, 4.618802153517012066, -3.433295621305382905 ) ) ;
#1771=LINE ( 'NONE', #15201, #16938 ) ;
#1830=ORIENTED_EDGE ( 'NONE', *, *, #19679, .T. ) ;
#1831=EDGE_CURVE ( 'NONE', #9606, #13337, #14784, .T. ) ;
#1832=CARTESIAN_POINT ( 'NONE',  ( 0.000000000000000000, 0.000000000000000000, -5.000000000000000000 ) ) ;
#1836=CARTESIAN_POINT ( 'NONE',  ( 4.197478902586992966, -0.8524102783748346290, -3.505063281295504041 ) ) ;
#1944=ORIENTED_EDGE ( 'NONE', *, *, #8240, .T. ) ;
#1966=CARTESIAN_POINT ( 'NONE',  ( -6.473970235329672780E-16, -4.862606272033106691, -3.745885042887442395 ) ) ;
#2000=ORIENTED_EDGE ( 'NONE', *, *, #13822, .F. ) ;
#2024=PRODUCT_DEFINITION_CONTEXT ( 'detailed design', #19698, 'design' ) ;
#2030=ORIENTED_EDGE ( 'NONE', *, *, #6055, .F. ) ;
#2064=B_SPLINE_CURVE_WITH_KNOTS ( 'NONE', 3,
 ( #4053, #18658, #2494, #22291, #9881, #2125 ),
 .UNSPECIFIED., .F., .F.,
 ( 4, 2, 4 ),
 ( 0.002365888236228001588, 0.003551327329835089319, 0.004736766423442177049 ),
 .UNSPECIFIED. ) ;
#2078=CARTESIAN_POINT ( 'NONE',  ( 4.000000000000000000, -1.700175430507292473, -3.320327275037661785 ) ) ;
#2125=CARTESIAN_POINT ( 'NONE',  ( -4.000000000000000000, -2.309401076758515803, -0.4999999999999995559 ) ) ;
#2131=CARTESIAN_POINT ( 'NONE',  ( -1.240299975428113101E-15, -4.647091401871173311, -3.572172305156514849 ) ) ;
#2138=DIRECTION ( 'NONE',  ( 0.000000000000000000, 0.000000000000000000, 1.000000000000000000 ) ) ;
#2186=( BOUNDED_SURFACE ( )  B_SPLINE_SURFACE ( 3, 2, ( 
 ( #4668, #8533, #12082 ),
 ( #4419, #4895, #21206 ),
 ( #6822, #15779, #2598 ),
 ( #19611, #21431, #3078 ),
 ( #2734, #13757, #15554 ),
 ( #21079, #14220, #23363 ) ),
 .UNSPECIFIED., .F., .F., .F. ) 
 B_SPLINE_SURFACE_WITH_KNOTS ( ( 4, 2, 4 ),
 ( 3, 3 ),
 ( 0.02027752710269158445, 0.02273781595091097299, 0.02519810479913036153 ),
 ( 0.000000000000000000, 1.000000000000000000 ),
 .UNSPECIFIED. ) 
 GEOMETRIC_REPRESENTATION_ITEM ( )  RATIONAL_B_SPLINE_SURFACE ( (
 ( 1.000000000000000000, 0.8047781431712808242, 1.000000000000000000),
 ( 1.000000000000000000, 0.8123773247083928561, 1.000000000000000000),
 ( 1.000000000000000000, 0.8190670192154906326, 1.000000000000000000),
 ( 1.000000000000000000, 0.8192353552912178261, 1.000000000000000000),
 ( 1.000000000000000000, 0.8126132098226825917, 1.000000000000000000),
 ( 1.000000000000000000, 0.8047712465856394770, 1.000000000000000000) ) ) 
 REPRESENTATION_ITEM ( '' )  SURFACE ( )  );
#2268=MECHANICAL_DESIGN_GEOMETRIC_PRESENTATION_REPRESENTATION('',(#13888),#17346);
#2279=CARTESIAN_POINT ( 'NONE',  ( 4.000000000000000000, 0.000000000000000000, 0.000000000000000000 ) ) ;
#2300=FACE_OUTER_BOUND ( 'NONE', #14406, .T. ) ;
#2327=PLANE ( 'NONE',  #9596 ) ;
#2328=FACE_OUTER_BOUND ( 'NONE', #10229, .T. ) ;
#2338=DIRECTION ( 'NONE',  ( -1.000000000000000000, 0.000000000000000000, 0.000000000000000000 ) ) ;
#2359=CARTESIAN_POINT ( 'NONE',  ( 2.682243648011666703, 3.070208061305304881, -0.04852650426601266831 ) ) ;
#2368=ORIENTED_EDGE ( 'NONE', *, *, #6862, .T. ) ;
#2379=ORIENTED_EDGE ( 'NONE', *, *, #9781, .F. ) ;
#2391=PLANE ( 'NONE',  #4733 ) ;
#2395=CARTESIAN_POINT ( 'NONE',  ( 0.000000000000000000, 0.000000000000000000, 0.000000000000000000 ) ) ;
#2445=CONICAL_SURFACE ( 'NONE', #9412, 4.000000000000000000, 0.8911886515913786111 ) ;
#2494=CARTESIAN_POINT ( 'NONE',  ( -2.682243648011671588, -3.070208061305317759, -0.04852650426602272971 ) ) ;
#2541=B_SPLINE_CURVE_WITH_KNOTS ( 'NONE', 3,
 ( #14118, #3096, #15798, #15568, #1033 ),
 .UNSPECIFIED., .F., .F.,
 ( 4, 1, 4 ),
 ( 0.000000000000000000, 0.002309401076758505356, 0.004618802153517010713 ),
 .UNSPECIFIED. ) ;
#2553=ORIENTED_EDGE ( 'NONE', *, *, #3097, .F. ) ;
#2584=EDGE_LOOP ( 'NONE', ( #14668, #14902, #12639, #2722, #11589 ) ) ;
#2590=DIRECTION ( 'NONE',  ( 0.5000000000000022204, 0.8660254037844374864, -0.000000000000000000 ) ) ;
#2592=CARTESIAN_POINT ( 'NONE',  ( -1.391697335622809950, -4.043246145443391448, -3.503898532754372575 ) ) ;
#2596=SURFACE_STYLE_USAGE ( .BOTH. , #10225 ) ;
#2598=CARTESIAN_POINT ( 'NONE',  ( -4.197477534772231955, 0.8522413273724368521, -3.505042416683225692 ) ) ;
#2610=AXIS2_PLACEMENT_3D ( 'NONE', #21430, #4667, #15778 ) ;
#2630=VECTOR ( 'NONE', #15357, 1000.000000000000000 ) ;
#2659=PLANE ( 'NONE',  #4593 ) ;
#2700=ORIENTED_EDGE ( 'NONE', *, *, #15773, .T. ) ;
#2722=ORIENTED_EDGE ( 'NONE', *, *, #14313, .T. ) ;
#2729=CARTESIAN_POINT ( 'NONE',  ( 0.000000000000000000, 0.000000000000000000, 0.000000000000000000 ) ) ;
#2734=CARTESIAN_POINT ( 'NONE',  ( -4.000000000000000000, -1.680117682357936904, -3.316611593218794951 ) ) ;
#2770=CARTESIAN_POINT ( 'NONE',  ( 0.5449313310647804220, 4.304185902836899835, -3.316620875263383894 ) ) ;
#2774=ORIENTED_EDGE ( 'NONE', *, *, #15773, .F. ) ;
#2872=ORIENTED_EDGE ( 'NONE', *, *, #6862, .F. ) ;
#2953=CARTESIAN_POINT ( 'NONE',  ( 2.499999999999999556, 0.000000000000000000, 3.469446951953614189E-15 ) ) ;
#2961=ORIENTED_EDGE ( 'NONE', *, *, #18419, .T. ) ;
#2985=ORIENTED_EDGE ( 'NONE', *, *, #3854, .F. ) ;
#3006=VECTOR ( 'NONE', #22601, 1000.000000000000000 ) ;
#3012=ORIENTED_EDGE ( 'NONE', *, *, #17601, .F. ) ;
#3078=CARTESIAN_POINT ( 'NONE',  ( -4.197312064133472020, -0.8182229787990021874, -3.502518405183886685 ) ) ;
#3096=CARTESIAN_POINT ( 'NONE',  ( -3.333333333333332149, -2.694301256218264218, -3.300726591567082036 ) ) ;
#3097=EDGE_CURVE ( 'NONE', #16162, #21528, #2541, .T. ) ;
#3105=CARTESIAN_POINT ( 'NONE',  ( -5.560781378645573980, 0.000000000000000000, -4.000000000000000000 ) ) ;
#3128=CARTESIAN_POINT ( 'NONE',  ( -4.154094228333736538, -2.398367420967545627, -3.721909803043222276 ) ) ;
#3172=CARTESIAN_POINT ( 'NONE',  ( -0.5636800770129166693, -4.293361309317430319, -3.531542292955206275 ) ) ;
#3198=CARTESIAN_POINT ( 'NONE',  ( -4.000000000000000000, -2.309401076758512694, -3.433295621305382461 ) ) ;
#3223=B_SPLINE_CURVE_WITH_KNOTS ( 'NONE', 3,
 ( #19930, #16436, #23786, #21986, #20161, #18947, #17277, #20517 ),
 .UNSPECIFIED., .F., .F.,
 ( 4, 2, 2, 4 ),
 ( 2.465131517075058656E-07, 0.001183067374689851080, 0.001774477805458923299, 0.002365888236227995517 ),
 .UNSPECIFIED. ) ;
#3264=B_SPLINE_CURVE_WITH_KNOTS ( 'NONE', 3,
 ( #18704, #9437, #15129, #9553, #5453, #16917, #251, #14879 ),
 .UNSPECIFIED., .F., .F.,
 ( 4, 2, 2, 4 ),
 ( 2.465131517071610173E-07, 0.001183067374689837636, 0.001774477805458902699, 0.002365888236227967761 ),
 .UNSPECIFIED. ) ;
#3300=CARTESIAN_POINT ( 'NONE',  ( -4.211140560182196957, 2.431303136016537803, -3.745885042887433514 ) ) ;
#3307=CARTESIAN_POINT ( 'NONE',  ( -2.725741868435985094, 3.045094352034055429, -3.220599429844047012 ) ) ;
#3315=CONICAL_SURFACE ( 'NONE', #19911, 5.560781378645573980, 1.221730476396046816 ) ;
#3327=DIRECTION ( 'NONE',  ( 1.000000000000000000, 0.000000000000000000, 0.000000000000000000 ) ) ;
#3329=CARTESIAN_POINT ( 'NONE',  ( -6.259644161404860030E-16, -4.618802153517027165, -5.000000000000000000 ) ) ;
#3353=CONICAL_SURFACE ( 'NONE', #17252, 4.000000000000000000, 0.8911886515913786111 ) ;
#3450=B_SPLINE_CURVE_WITH_KNOTS ( 'NONE', 3,
 ( #7520, #14912, #5127, #61, #1496, #3300 ),
 .UNSPECIFIED., .F., .F.,
 ( 4, 2, 4 ),
 ( 0.002452478801916376308, 0.003676905084148007850, 0.004901331366379639391 ),
 .UNSPECIFIED. ) ;
#3476=DIRECTION ( 'NONE',  ( 0.000000000000000000, 0.000000000000000000, -1.000000000000000000 ) ) ;
#3485=VERTEX_POINT ( 'NONE', #2953 ) ;
#3488=CIRCLE ( 'NONE', #20829, 2.500000000000000888 ) ;
#3492=CARTESIAN_POINT ( 'NONE',  ( 3.333333333333332593, 2.694301256218250007, -3.300726591567078483 ) ) ;
#3548=VECTOR ( 'NONE', #22573, 1000.000000000000000 ) ;
#3555=CARTESIAN_POINT ( 'NONE',  ( 0.6666666666666658525, -4.233901974057276085, -3.300726591567086476 ) ) ;
#3561=DIRECTION ( 'NONE',  ( -0.000000000000000000, -0.000000000000000000, 1.000000000000000000 ) ) ;
#3586=CARTESIAN_POINT ( 'NONE',  ( -4.101948962585906244, 2.368261337751074169, -3.681124513963621503 ) ) ;
#3607=CARTESIAN_POINT ( 'NONE',  ( -1.274258131565027874, -3.883108878240886241, -3.220599429844051009 ) ) ;
#3639=LINE ( 'NONE', #14904, #13374 ) ;
#3643=CARTESIAN_POINT ( 'NONE',  ( 4.000000000000000888, -0.8578082829538523635, -3.433262215449808696 ) ) ;
#3652=CARTESIAN_POINT ( 'NONE',  ( -4.141042297810615835, 2.227970268150415656, -3.687027686973619822 ) ) ;
#3678=CARTESIAN_POINT ( 'NONE',  ( 3.999999999999999112, 2.309401076758497595, -3.504271511726784194 ) ) ;
#3679=CARTESIAN_POINT ( 'NONE',  ( 2.000000000000005329, -3.464101615137751722, 0.000000000000000000 ) ) ;
#3696=CARTESIAN_POINT ( 'NONE',  ( -4.000000000000000000, 1.941961291383472732, -0.3515519931180205448 ) ) ;
#3721=ORIENTED_EDGE ( 'NONE', *, *, #14896, .F. ) ;
#3726=DIRECTION ( 'NONE',  ( 0.8191520442889902442, 1.003171929053522651E-16, -0.5735764363510482688 ) ) ;
#3727=CARTESIAN_POINT ( 'NONE',  ( -4.175002511812151873, -2.208363329454905877, -3.469254087858246738 ) ) ;
#3749=VERTEX_POINT ( 'NONE', #19717 ) ;
#3751=ORIENTED_EDGE ( 'NONE', *, *, #10525, .T. ) ;
#3766=CARTESIAN_POINT ( 'NONE',  ( 4.000000000000000000, 0.8378280264232961239, -3.220590601395640018 ) ) ;
#3769=DIRECTION ( 'NONE',  ( 1.000000000000000000, 0.000000000000000000, 0.000000000000000000 ) ) ;
#3779=CARTESIAN_POINT ( 'NONE',  ( 0.000000000000000000, 0.000000000000000000, -5.000000000000000888 ) ) ;
#3795=CONICAL_SURFACE ( 'NONE', #14266, 4.000000000000000000, 0.8911886515913786111 ) ;
#3829=CARTESIAN_POINT ( 'NONE',  ( 2.500000000000000444, 0.000000000000000000, -5.000000000000000888 ) ) ;
#3831=CARTESIAN_POINT ( 'NONE',  ( -6.473970235329672780E-16, -4.862606272033106691, -3.745885042887442395 ) ) ;
#3841=CARTESIAN_POINT ( 'NONE',  ( 2.000000000000000444, 3.464101615137754830, -3.142992957459231018 ) ) ;
#3843=CIRCLE ( 'NONE', #20810, 5.384454397937118664 ) ;
#3854=EDGE_CURVE ( 'NONE', #9508, #18021, #6573, .T. ) ;
#3861=VECTOR ( 'NONE', #453, 1000.000000000000000 ) ;
#3880=DIRECTION ( 'NONE',  ( -0.000000000000000000, -0.000000000000000000, 1.000000000000000000 ) ) ;
#3885=EDGE_LOOP ( 'NONE', ( #23721, #7361 ) ) ;
#3921=CARTESIAN_POINT ( 'NONE',  ( -4.000000000000000000, -0.3979232138631226823, -3.896351557369779711E-17 ) ) ;
#3940=ORIENTED_EDGE ( 'NONE', *, *, #18670, .T. ) ;
#3948=DIRECTION ( 'NONE',  ( -1.000000000000000000, 0.000000000000000000, 0.000000000000000000 ) ) ;
#3975=EDGE_CURVE ( 'NONE', #19949, #4882, #11195, .T. ) ;
#3989=EDGE_LOOP ( 'NONE', ( #21774, #10519, #8095, #13614 ) ) ;
#4039=MANIFOLD_SOLID_BREP ( 'EndChamfer', #14496 ) ;
#4053=CARTESIAN_POINT ( 'NONE',  ( -2.000000000000007550, -3.464101615137749945, 0.000000000000000000 ) ) ;
#4086=CARTESIAN_POINT ( 'NONE',  ( -4.000000000000000000, 0.000000000000000000, 0.000000000000000000 ) ) ;
#4089=CARTESIAN_POINT ( 'NONE',  ( -0.1410422978106123659, 4.700232962125094893, -3.687027686973624707 ) ) ;
#4099=EDGE_CURVE ( 'NONE', #13534, #13282, #972, .T. ) ;
#4125=CARTESIAN_POINT ( 'NONE',  ( -4.211140560182196957, 2.431303136016537803, -3.745885042887433514 ) ) ;
#4144=DIRECTION ( 'NONE',  ( -1.000000000000000000, 0.000000000000000000, 0.000000000000000000 ) ) ;
#4163=CARTESIAN_POINT ( 'NONE',  ( 2.000000000000008882, 3.464101615137749945, 0.000000000000000000 ) ) ;
#4170=AXIS2_PLACEMENT_3D ( 'NONE', #16262, #5487, #16475 ) ;
#4173=CARTESIAN_POINT ( 'NONE',  ( 1.567478505476134606E-15, 4.618802153517012066, -5.000000000000000000 ) ) ;
#4182=AXIS2_PLACEMENT_3D ( 'NONE', #5983, #22872, #20705 ) ;
#4267=CARTESIAN_POINT ( 'NONE',  ( -6.473970235329672780E-16, -4.862606272033106691, -3.745885042887442395 ) ) ;
#4289=CARTESIAN_POINT ( 'NONE',  ( -5.384454397937118664, 6.702023979852544604E-16, -5.000000000000000000 ) ) ;
#4295=CARTESIAN_POINT ( 'NONE',  ( -0.6448876103708541807, -4.246476118072358474, -0.2256878752776773356 ) ) ;
#4305=EDGE_CURVE ( 'NONE', #9606, #12, #16322, .T. ) ;
#4334=DIRECTION ( 'NONE',  ( 0.8660254037844374864, -0.5000000000000018874, 0.000000000000000000 ) ) ;
#4335=EDGE_CURVE ( 'NONE', #1398, #4834, #7020, .T. ) ;
#4386=CARTESIAN_POINT ( 'NONE',  ( 0.000000000000000000, 0.000000000000000000, 0.000000000000000000 ) ) ;
#4407=CARTESIAN_POINT ( 'NONE',  ( -1.828356344711647319, -3.563200125723192002, -1.076197711133951296E-14 ) ) ;
#4419=CARTESIAN_POINT ( 'NONE',  ( -4.000000000000000000, 1.700094919196744270, -3.320312364301766017 ) ) ;
#4451=CARTESIAN_POINT ( 'NONE',  ( -4.000000000000000000, -2.309401076758512694, -5.000000000000000000 ) ) ;
#4456=ORIENTED_EDGE ( 'NONE', *, *, #7402, .F. ) ;
#4466=CARTESIAN_POINT ( 'NONE',  ( -4.000000000000000000, -2.309401076758512694, -3.433295621305382461 ) ) ;
#4471=CARTESIAN_POINT ( 'NONE',  ( 3.540020015735602765, 2.810662092924382627, -3.602146406945867962 ) ) ;
#4483=ORIENTED_EDGE ( 'NONE', *, *, #14896, .T. ) ;
#4529=CARTESIAN_POINT ( 'NONE',  ( -2.804994570502171047, -3.229033611042465335, -3.526374918436838701 ) ) ;
#4546=CARTESIAN_POINT ( 'NONE',  ( -2.171643655288372443, 3.365003104552320767, 2.541098841762897165E-18 ) ) ;
#4568=ORIENTED_EDGE ( 'NONE', *, *, #6949, .T. ) ;
#4593=AXIS2_PLACEMENT_3D ( 'NONE', #7980, #22700, #13330 ) ;
#4599=EDGE_CURVE ( 'NONE', #3749, #16162, #6439, .T. ) ;
#4663=DIRECTION ( 'NONE',  ( -0.000000000000000000, 0.000000000000000000, -1.000000000000000000 ) ) ;
#4667=DIRECTION ( 'NONE',  ( 0.000000000000000000, 0.000000000000000000, -1.000000000000000000 ) ) ;
#4668=CARTESIAN_POINT ( 'NONE',  ( -4.000000000000000000, 2.511478553582031203, -3.469254451724764543 ) ) ;
#4669=ORIENTED_EDGE ( 'NONE', *, *, #14313, .F. ) ;
#4709=CARTESIAN_POINT ( 'NONE',  ( 2.725741868436127202, -3.045094352033990148, -3.220599429844051453 ) ) ;
#4724=EDGE_LOOP ( 'NONE', ( #16323, #23364, #21725 ) ) ;
#4733=AXIS2_PLACEMENT_3D ( 'NONE', #20500, #3948, #2138 ) ;
#4817=B_SPLINE_CURVE_WITH_KNOTS ( 'NONE', 3,
 ( #13690, #9795, #21009, #10052 ),
 .UNSPECIFIED., .F., .F.,
 ( 4, 4 ),
 ( 0.000000000000000000, 0.002452478801916361129 ),
 .UNSPECIFIED. ) ;
#4829=DIRECTION ( 'NONE',  ( 0.000000000000000000, 0.000000000000000000, -1.000000000000000000 ) ) ;
#4834=VERTEX_POINT ( 'NONE', #7790 ) ;
#4836=CARTESIAN_POINT ( 'NONE',  ( 4.000000000000000000, -2.309401076758516691, -0.4999999999999995559 ) ) ;
#4882=VERTEX_POINT ( 'NONE', #4289 ) ;
#4895=CARTESIAN_POINT ( 'NONE',  ( -4.000000000000000000, 1.677772373332757194, -3.535253723897187506 ) ) ;
#4899=ORIENTED_EDGE ( 'NONE', *, *, #22306, .F. ) ;
#4906=CARTESIAN_POINT ( 'NONE',  ( 4.211140560182196957, -2.431303136016555122, -3.745885042887436622 ) ) ;
#4945=CARTESIAN_POINT ( 'NONE',  ( 0.000000000000000000, 0.000000000000000000, 0.000000000000000000 ) ) ;
#5007=CARTESIAN_POINT ( 'NONE',  ( -2.756197834950067094, -3.027510591568735254, -3.223146290109809797 ) ) ;
#5018=VECTOR ( 'NONE', #15077, 1000.000000000000000 ) ;
#5019=CARTESIAN_POINT ( 'NONE',  ( 1.567478505476134606E-15, 4.618802153517012066, -5.000000000000000000 ) ) ;
#5094=CARTESIAN_POINT ( 'NONE',  ( -1.655952806101422814, 3.662737355149034979, -7.623296525288699970E-18 ) ) ;
#5095=EDGE_CURVE ( 'NONE', #10369, #6737, #3639, .T. ) ;
#5127=CARTESIAN_POINT ( 'NONE',  ( -4.198928548860774157, 0.8158838809860065044, -3.526471437616918170 ) ) ;
#5133=CARTESIAN_POINT ( 'NONE',  ( -1.243802165048909503, 3.900692638707381921, -3.223146290109805800 ) ) ;
#5153=FACE_OUTER_BOUND ( 'NONE', #14025, .T. ) ;
#5163=ADVANCED_FACE ( 'NONE', ( #20435 ), #19957, .F. ) ;
#5212=CARTESIAN_POINT ( 'NONE',  ( 0.000000000000000000, 0.000000000000000000, -4.484454397937119197 ) ) ;
#5252=FACE_OUTER_BOUND ( 'NONE', #5264, .T. ) ;
#5254=DIRECTION ( 'NONE',  ( -1.000000000000000000, 0.000000000000000000, 0.000000000000000000 ) ) ;
#5264=EDGE_LOOP ( 'NONE', ( #15057, #3012, #2985, #7404 ) ) ;
#5265=CARTESIAN_POINT ( 'NONE',  ( 0.000000000000000000, 0.000000000000000000, -4.694516984716113228 ) ) ;
#5281=ORIENTED_EDGE ( 'NONE', *, *, #20668, .T. ) ;
#5298=DIRECTION ( 'NONE',  ( -1.000000000000000000, 0.000000000000000000, 0.000000000000000000 ) ) ;
#5339=DIRECTION ( 'NONE',  ( 1.000000000000000000, 0.000000000000000000, 0.000000000000000000 ) ) ;
#5355=ORIENTED_EDGE ( 'NONE', *, *, #11732, .F. ) ;
#5401=VERTEX_POINT ( 'NONE', #23074 ) ;
#5407=CARTESIAN_POINT ( 'NONE',  ( 0.000000000000000000, 0.000000000000000000, -0.2800830152838844622 ) ) ;
#5423=AXIS2_PLACEMENT_3D ( 'NONE', #14429, #14899, #22009 ) ;
#5427=EDGE_CURVE ( 'NONE', #18124, #11437, #8411, .T. ) ;
#5446=CARTESIAN_POINT ( 'NONE',  ( -3.453038570459499024, -2.625189405340453419, -3.535263753545272891 ) ) ;
#5453=CARTESIAN_POINT ( 'NONE',  ( 2.687328764639642653, -3.067272167851299969, -0.05923475698271395140 ) ) ;
#5457=EDGE_LOOP ( 'NONE', ( #8212, #20052, #4669 ) ) ;
#5478=CARTESIAN_POINT ( 'NONE',  ( 4.000000000000000000, -2.471525695159793035, -3.686886880705770864 ) ) ;
#5483=DIRECTION ( 'NONE',  ( 1.000000000000000000, 0.000000000000000000, 0.000000000000000000 ) ) ;
#5485=EDGE_LOOP ( 'NONE', ( #21783, #1830, #23423, #18020, #388 ) ) ;
#5487=DIRECTION ( 'NONE',  ( 0.000000000000000000, 0.000000000000000000, -1.000000000000000000 ) ) ;
#5498=CARTESIAN_POINT ( 'NONE',  ( 0.000000000000000000, 0.000000000000000000, -4.694516984716113228 ) ) ;
#5524=CARTESIAN_POINT ( 'NONE',  ( -4.000000000000000000, 0.1981133338132459731, 2.096406544454392723E-17 ) ) ;
#5587=SHAPE_REPRESENTATION ( 'hex flange nut gradea_iso_ISO - 4161 - M5 - N', ( #11210 ), #13515 ) ;
#5618=EDGE_CURVE ( 'NONE', #11437, #160, #3223, .T. ) ;
#5647=ORIENTED_EDGE ( 'NONE', *, *, #20190, .T. ) ;
#5729=( BOUNDED_SURFACE ( )  B_SPLINE_SURFACE ( 3, 2, ( 
 ( #3727, #9193, #9072 ),
 ( #1253, #5446, #15998 ),
 ( #5007, #23103, #21983 ),
 ( #3607, #14635, #16434 ),
 ( #10330, #3172, #13981 ),
 ( #12170, #21304, #11026 ) ),
 .UNSPECIFIED., .F., .F., .F. ) 
 B_SPLINE_SURFACE_WITH_KNOTS ( ( 4, 2, 4 ),
 ( 3, 3 ),
 ( 0.02032853247518126918, 0.02278863295364821906, 0.02524873343211516893 ),
 ( 0.000000000000000000, 1.000000000000000000 ),
 .UNSPECIFIED. ) 
 GEOMETRIC_REPRESENTATION_ITEM ( )  RATIONAL_B_SPLINE_SURFACE ( (
 ( 1.000000000000000000, 0.8047781615896838492, 1.000000000000000000),
 ( 1.000000000000000000, 0.8123767586288186404, 1.000000000000000000),
 ( 1.000000000000000000, 0.8190662415565814758, 1.000000000000000000),
 ( 1.000000000000000000, 0.8192361015667604107, 1.000000000000000000),
 ( 1.000000000000000000, 0.8126135807104967190, 1.000000000000000000),
 ( 1.000000000000000000, 0.8047712338318580017, 1.000000000000000000) ) ) 
 REPRESENTATION_ITEM ( '' )  SURFACE ( )  );
#5792=FACE_OUTER_BOUND ( 'NONE', #5485, .T. ) ;
#5796=CARTESIAN_POINT ( 'NONE',  ( 0.000000000000000000, 0.000000000000000000, -4.484454397937119197 ) ) ;
#5825=DIRECTION ( 'NONE',  ( 1.000000000000000000, 0.000000000000000000, 0.000000000000000000 ) ) ;
#5838=CARTESIAN_POINT ( 'NONE',  ( -1.747541505913277282, 3.837784562140256650, -3.503702292528906526 ) ) ;
#5863=CARTESIAN_POINT ( 'NONE',  ( -2.100000000000000089, 2.571758278209441957E-16, -5.000000000000000000 ) ) ;
#5865=ADVANCED_FACE ( 'NONE', ( #15599 ), #21322, .F. ) ;
#5866=CARTESIAN_POINT ( 'NONE',  ( -4.000000000000000000, -1.942223658245633811, -0.3516579909967644246 ) ) ;
#5880=DIRECTION ( 'NONE',  ( 0.8191520442889875797, 0.000000000000000000, 0.5735764363510522656 ) ) ;
#5897=VERTEX_POINT ( 'NONE', #18443 ) ;
#5956=ORIENTED_EDGE ( 'NONE', *, *, #20695, .T. ) ;
#5983=CARTESIAN_POINT ( 'NONE',  ( 0.000000000000000000, 0.000000000000000000, 0.000000000000000000 ) ) ;
#5984=AXIS2_PLACEMENT_3D ( 'NONE', #2395, #20740, #6146 ) ;
#5988=CIRCLE ( 'NONE', #18685, 0.5155456020628804703 ) ;
#6055=EDGE_CURVE ( 'NONE', #6737, #4834, #3488, .T. ) ;
#6103=FACE_OUTER_BOUND ( 'NONE', #22912, .T. ) ;
#6108=CARTESIAN_POINT ( 'NONE',  ( -2.000000000000007550, -3.464101615137749945, 0.000000000000000000 ) ) ;
#6146=DIRECTION ( 'NONE',  ( -1.000000000000000000, 0.000000000000000000, 0.000000000000000000 ) ) ;
#6192=ORIENTED_EDGE ( 'NONE', *, *, #13021, .T. ) ;
#6238=( NAMED_UNIT ( * ) PLANE_ANGLE_UNIT ( ) SI_UNIT ( $, .RADIAN. ) );
#6241=LINE ( 'NONE', #205, #5018 ) ;
#6253=CARTESIAN_POINT ( 'NONE',  ( -4.000000000000000000, 2.309401076758498483, -0.4999999999999927280 ) ) ;
#6268=FACE_OUTER_BOUND ( 'NONE', #14302, .T. ) ;
#6283=CARTESIAN_POINT ( 'NONE',  ( -0.02511973781850462134, 4.877415612947412882, -3.751298745799839462 ) ) ;
#6321=ADVANCED_FACE ( 'NONE', ( #5153 ), #10810, .F. ) ;
#6328=ORIENTED_EDGE ( 'NONE', *, *, #10525, .F. ) ;
#6341=FACE_OUTER_BOUND ( 'NONE', #21118, .T. ) ;
#6355=VECTOR ( 'NONE', #7477, 1000.000000000000000 ) ;
#6368=( BOUNDED_SURFACE ( )  B_SPLINE_SURFACE ( 3, 2, ( 
 ( #9918, #17402, #12008 ),
 ( #22815, #22689, #4471 ),
 ( #11877, #379, #841 ),
 ( #15484, #19311, #19185 ),
 ( #2770, #20756, #7851 ),
 ( #22566, #4089, #6283 ) ),
 .UNSPECIFIED., .F., .F., .F. ) 
 B_SPLINE_SURFACE_WITH_KNOTS ( ( 4, 2, 4 ),
 ( 3, 3 ),
 ( 0.02032853247518126225, 0.02278863295364821212, 0.02524873343211516200 ),
 ( 0.000000000000000000, 1.000000000000000000 ),
 .UNSPECIFIED. ) 
 GEOMETRIC_REPRESENTATION_ITEM ( )  RATIONAL_B_SPLINE_SURFACE ( (
 ( 1.000000000000000000, 0.8047781615896835161, 1.000000000000000000),
 ( 1.000000000000000000, 0.8123767586291043008, 1.000000000000000000),
 ( 1.000000000000000000, 0.8190662415562011134, 1.000000000000000000),
 ( 1.000000000000000000, 0.8192361015671398849, 1.000000000000000000),
 ( 1.000000000000000000, 0.8126135807102121689, 1.000000000000000000),
 ( 1.000000000000000000, 0.8047712338318585568, 1.000000000000000000) ) ) 
 REPRESENTATION_ITEM ( '' )  SURFACE ( )  );
#6399=ADVANCED_FACE ( 'NONE', ( #6103 ), #20008, .T. ) ;
#6439=B_SPLINE_CURVE_WITH_KNOTS ( 'NONE', 3,
 ( #15705, #3128, #19307, #13686, #21005, #4466 ),
 .UNSPECIFIED., .F., .F.,
 ( 4, 2, 4 ),
 ( -3.640115492409406142E-06, 0.0002066546034006526487, 0.0004169493222937146744 ),
 .UNSPECIFIED. ) ;
#6555=AXIS2_PLACEMENT_3D ( 'NONE', #23761, #20495, #22068 ) ;
#6573=B_SPLINE_CURVE_WITH_KNOTS ( 'NONE', 3,
 ( #10823, #9098, #8984, #20081, #8875, #14666 ),
 .UNSPECIFIED., .F., .F.,
 ( 4, 2, 4 ),
 ( -3.640115492407174633E-06, 0.0002066546034006553863, 0.0004169493222937179812 ),
 .UNSPECIFIED. ) ;
#6594=PRESENTATION_STYLE_ASSIGNMENT (( #2596 ) ) ;
#6598=ADVANCED_FACE ( 'NONE', ( #17219 ), #1118, .T. ) ;
#6614=ORIENTED_EDGE ( 'NONE', *, *, #9386, .T. ) ;
#6634=DIRECTION ( 'NONE',  ( 0.000000000000000000, 0.000000000000000000, -1.000000000000000000 ) ) ;
#6645=CARTESIAN_POINT ( 'NONE',  ( 4.141042297810615835, -2.227970268150433863, -3.687027686973623819 ) ) ;
#6693=FACE_OUTER_BOUND ( 'NONE', #6722, .T. ) ;
#6714=ADVANCED_BREP_SHAPE_REPRESENTATION ( '', ( #4039, #11210 ), #13515 ) ;
#6718=CARTESIAN_POINT ( 'NONE',  ( 4.154306624731035846, -2.398490048085128556, -3.721999068284417955 ) ) ;
#6720=EDGE_LOOP ( 'NONE', ( #18678, #12247, #11215, #14766, #7216 ) ) ;
#6722=EDGE_LOOP ( 'NONE', ( #20683, #6328, #4483, #17792 ) ) ;
#6727=CARTESIAN_POINT ( 'NONE',  ( 4.000000000000000000, -2.309401076758514915, -3.433295621305383349 ) ) ;
#6737=VERTEX_POINT ( 'NONE', #12747 ) ;
#6759=CARTESIAN_POINT ( 'NONE',  ( -0.02448733951239248641, -4.877042772274742255, -3.751161874094027571 ) ) ;
#6787=ORIENTED_EDGE ( 'NONE', *, *, #9762, .F. ) ;
#6788=CARTESIAN_POINT ( 'NONE',  ( -6.259644161404860030E-16, -4.618802153517027165, -3.433295621305388234 ) ) ;
#6822=CARTESIAN_POINT ( 'NONE',  ( -4.000000000000000000, 0.8730739991738342143, -3.223134629628428893 ) ) ;
#6842=CARTESIAN_POINT ( 'NONE',  ( 3.999999999999999112, -1.539600717839012978, -3.300726591567080703 ) ) ;
#6862=EDGE_CURVE ( 'NONE', #16162, #12107, #16915, .T. ) ;
#6885=ORIENTED_EDGE ( 'NONE', *, *, #23478, .T. ) ;
#6925=ORIENTED_EDGE ( 'NONE', *, *, #7030, .F. ) ;
#6949=EDGE_CURVE ( 'NONE', #21209, #8518, #7390, .T. ) ;
#6977=AXIS2_PLACEMENT_3D ( 'NONE', #5212, #21751, #18015 ) ;
#7020=LINE ( 'NONE', #20158, #8695 ) ;
#7030=EDGE_CURVE ( 'NONE', #20231, #8518, #19274, .T. ) ;
#7051=B_SPLINE_CURVE_WITH_KNOTS ( 'NONE', 3,
 ( #16602, #57, #16352, #11307, #11187, #19961, #18514, #1966 ),
 .UNSPECIFIED., .F., .F.,
 ( 4, 2, 2, 4 ),
 ( 0.000000000000000000, 0.002450665683189819262, 0.003675998524784728893, 0.004901331366379639391 ),
 .UNSPECIFIED. ) ;
#7057=CARTESIAN_POINT ( 'NONE',  ( -3.436319922987618902, 2.634841920961291439, -3.531542292955721862 ) ) ;
#7086=DIRECTION ( 'NONE',  ( 0.000000000000000000, 0.000000000000000000, 1.000000000000000000 ) ) ;
#7089=B_SPLINE_CURVE_WITH_KNOTS ( 'NONE', 3,
 ( #20373, #3492, #3841, #11257, #20146 ),
 .UNSPECIFIED., .F., .F.,
 ( 4, 1, 4 ),
 ( 0.000000000000000000, 0.002309401076758505356, 0.004618802153517010713 ),
 .UNSPECIFIED. ) ;
#7104=CARTESIAN_POINT ( 'NONE',  ( 0.000000000000000000, 0.000000000000000000, 0.000000000000000000 ) ) ;
#7118=CARTESIAN_POINT ( 'NONE',  ( -4.000000000000000000, 2.309401076758498483, -0.4999999999999927280 ) ) ;
#7155=AXIS2_PLACEMENT_3D ( 'NONE', #1832, #14546, #22013 ) ;
#7181=CARTESIAN_POINT ( 'NONE',  ( 0.000000000000000000, 0.000000000000000000, -4.974599999999998801 ) ) ;
#7215=FACE_OUTER_BOUND ( 'NONE', #5457, .T. ) ;
#7216=ORIENTED_EDGE ( 'NONE', *, *, #19679, .F. ) ;
#7222=CARTESIAN_POINT ( 'NONE',  ( 4.000000000000000000, -1.942223658245635809, -0.3516579909967643691 ) ) ;
#7288=AXIS2_PLACEMENT_3D ( 'NONE', #11448, #13034, #9623 ) ;
#7298=CARTESIAN_POINT ( 'NONE',  ( -4.175648173966055587, 2.207990556236529844, -3.469390959564062626 ) ) ;
#7316=CARTESIAN_POINT ( 'NONE',  ( -3.999999999999999112, 1.539600717838996324, -3.300726591567078039 ) ) ;
#7328=CARTESIAN_POINT ( 'NONE',  ( 1.655952806101427033, -3.662737355149048302, -1.182683869819604841E-14 ) ) ;
#7361=ORIENTED_EDGE ( 'NONE', *, *, #14479, .F. ) ;
#7363=EDGE_CURVE ( 'NONE', #12, #1352, #16885, .T. ) ;
#7385=ORIENTED_EDGE ( 'NONE', *, *, #15510, .T. ) ;
#7390=B_SPLINE_CURVE_WITH_KNOTS ( 'NONE', 3,
 ( #4086, #5524, #16646, #9159, #18554, #14726, #3696, #11348 ),
 .UNSPECIFIED., .F., .F.,
 ( 4, 2, 2, 4 ),
 ( 0.005725059856848641743, 0.006314084072593626612, 0.006903108288338611481, 0.008081156719828581220 ),
 .UNSPECIFIED. ) ;
#7393=ORIENTED_EDGE ( 'NONE', *, *, #1470, .F. ) ;
#7396=EDGE_CURVE ( 'NONE', #5897, #18021, #7089, .T. ) ;
#7402=EDGE_CURVE ( 'NONE', #15759, #7620, #10899, .T. ) ;
#7404=ORIENTED_EDGE ( 'NONE', *, *, #20190, .F. ) ;
#7410=CARTESIAN_POINT ( 'NONE',  ( 4.000000000000000000, -2.511475576507276042, -3.469253905236643565 ) ) ;
#7442=DIRECTION ( 'NONE',  ( 1.000000000000000000, 0.000000000000000000, 0.000000000000000000 ) ) ;
#7477=DIRECTION ( 'NONE',  ( 0.000000000000000000, 0.000000000000000000, 1.000000000000000000 ) ) ;
#7520=CARTESIAN_POINT ( 'NONE',  ( -4.197393957002303999, -7.773935952363655451E-14, -3.503767560748929810 ) ) ;
#7565=ADVANCED_FACE ( 'NONE', ( #5792 ), #2391, .F. ) ;
#7598=B_SPLINE_CURVE_WITH_KNOTS ( 'NONE', 3,
 ( #21920, #5866, #20473, #16632, #3921, #14825 ),
 .UNSPECIFIED., .F., .F.,
 ( 4, 2, 4 ),
 ( 0.003358874760055550156, 0.004541967308452096383, 0.005725059856848641743 ),
 .UNSPECIFIED. ) ;
#7610=CARTESIAN_POINT ( 'NONE',  ( 0.000000000000000000, 0.000000000000000000, -4.974599999999998801 ) ) ;
#7613=ADVANCED_FACE ( 'NONE', ( #13782 ), #10152, .T. ) ;
#7620=VERTEX_POINT ( 'NONE', #14129 ) ;
#7670=ORIENTED_EDGE ( 'NONE', *, *, #14092, .F. ) ;
#7690=( GEOMETRIC_REPRESENTATION_CONTEXT ( 3 ) GLOBAL_UNCERTAINTY_ASSIGNED_CONTEXT ( ( #16664 ) ) GLOBAL_UNIT_ASSIGNED_CONTEXT ( ( #20960, #6238, #15662 ) ) REPRESENTATION_CONTEXT ( 'NONE', 'WORKASPACE' ) );
#7781=ORIENTED_EDGE ( 'NONE', *, *, #10570, .T. ) ;
#7786=VERTEX_POINT ( 'NONE', #3679 ) ;
#7790=CARTESIAN_POINT ( 'NONE',  ( 2.500000000000000888, 3.061616997868384127E-16, -4.974599999999998801 ) ) ;
#7805=FILL_AREA_STYLE ('',( #9632 ) ) ;
#7851=CARTESIAN_POINT ( 'NONE',  ( 0.6810597143197052450, 4.461075778259290914, -3.598441714920602053 ) ) ;
#7861=CARTESIAN_POINT ( 'NONE',  ( -4.203833317240879275, -1.627343821129593859, -3.597273115243890818 ) ) ;
#7882=ORIENTED_EDGE ( 'NONE', *, *, #12035, .F. ) ;
#7914=CARTESIAN_POINT ( 'NONE',  ( 5.384454397937118664, 0.000000000000000000, -5.000000000000000000 ) ) ;
#7942=CARTESIAN_POINT ( 'NONE',  ( 4.197393957002303999, 7.772902908466098641E-14, -3.503767560748929810 ) ) ;
#7980=CARTESIAN_POINT ( 'NONE',  ( -4.000000000000000000, 2.309401076758498483, -5.000000000000000000 ) ) ;
#8013=EDGE_CURVE ( 'NONE', #7786, #23662, #15571, .T. ) ;
#8025=CARTESIAN_POINT ( 'NONE',  ( 0.000000000000000000, 0.000000000000000000, -5.000000000000000888 ) ) ;
#8026=CONICAL_SURFACE ( 'NONE', #19565, 2.059999999999998721, 0.9599310885968738161 ) ;
#8095=ORIENTED_EDGE ( 'NONE', *, *, #1831, .F. ) ;
#8172=CARTESIAN_POINT ( 'NONE',  ( 2.100000000000000089, 0.000000000000000000, -5.000000000000000000 ) ) ;
#8192=DIRECTION ( 'NONE',  ( 0.000000000000000000, 0.000000000000000000, 1.000000000000000000 ) ) ;
#8212=ORIENTED_EDGE ( 'NONE', *, *, #6949, .F. ) ;
#8214=VECTOR ( 'NONE', #12716, 999.9999999999998863 ) ;
#8240=EDGE_CURVE ( 'NONE', #3749, #10625, #23009, .T. ) ;
#8298=CARTESIAN_POINT ( 'NONE',  ( 4.101954839143059139, -2.368264730582948285, -3.681130640444269631 ) ) ;
#8332=CARTESIAN_POINT ( 'NONE',  ( 4.236525694536557474, -2.416953475386482530, -3.751298745799839462 ) ) ;
#8383=CYLINDRICAL_SURFACE ( 'NONE', #760, 2.500000000000000444 ) ;
#8385=ORIENTED_EDGE ( 'NONE', *, *, #7402, .T. ) ;
#8411=B_SPLINE_CURVE_WITH_KNOTS ( 'NONE', 3,
 ( #22949, #5094, #14173, #17524, #19561, #17889 ),
 .UNSPECIFIED., .F., .F.,
 ( 4, 2, 4 ),
 ( 0.002365888236227977302, 0.003551327329835078910, 0.004736766423442180518 ),
 .UNSPECIFIED. ) ;
#8459=CARTESIAN_POINT ( 'NONE',  ( 1.360585162435110629, -4.061296242128317857, -3.505054077164905024 ) ) ;
#8486=ORIENTED_EDGE ( 'NONE', *, *, #4099, .F. ) ;
#8502=CARTESIAN_POINT ( 'NONE',  ( 4.000000000000000000, 0.000000000000000000, 0.000000000000000000 ) ) ;
#8510=B_SPLINE_CURVE_WITH_KNOTS ( 'NONE', 3,
 ( #4163, #22402, #2359, #17097, #556, #9269 ),
 .UNSPECIFIED., .F., .F.,
 ( 4, 2, 4 ),
 ( 0.002365888236227995517, 0.003551327329835084114, 0.004736766423442172712 ),
 .UNSPECIFIED. ) ;
#8518=VERTEX_POINT ( 'NONE', #7118 ) ;
#8526=B_SPLINE_CURVE_WITH_KNOTS ( 'NONE', 3,
 ( #16849, #20950, #4295, #22512, #11698, #15654, #4407, #22983 ),
 .UNSPECIFIED., .F., .F.,
 ( 4, 2, 2, 4 ),
 ( 2.465131517390770070E-07, 0.001183067374689869946, 0.001774477805458935659, 0.002365888236228001588 ),
 .UNSPECIFIED. ) ;
#8533=CARTESIAN_POINT ( 'NONE',  ( -4.000000000000000000, 2.471528634177585282, -3.686887442155186712 ) ) ;
#8534=EDGE_LOOP ( 'NONE', ( #3751, #12530 ) ) ;
#8547=ADVANCED_FACE ( 'NONE', ( #13200 ), #16088, .T. ) ;
#8560=ORIENTED_EDGE ( 'NONE', *, *, #12858, .T. ) ;
#8652=CARTESIAN_POINT ( 'NONE',  ( 4.000000000000003553, -2.309401076758513138, -3.504271511726786859 ) ) ;
#8659=DIRECTION ( 'NONE',  ( 1.000000000000000000, 0.000000000000000000, 0.000000000000000000 ) ) ;
#8680=CARTESIAN_POINT ( 'NONE',  ( 1.411581201560190495E-15, 4.862606272033091592, -3.745885042887436622 ) ) ;
#8691=CARTESIAN_POINT ( 'NONE',  ( -4.000000000000004441, 2.309401076758496263, -3.504269196027523847 ) ) ;
#8695=VECTOR ( 'NONE', #3726, 1000.000000000000114 ) ;
#8768=CARTESIAN_POINT ( 'NONE',  ( 0.1750025118121568690, 4.719839900820621104, -3.469254087858248070 ) ) ;
#8778=DIRECTION ( 'NONE',  ( 1.000000000000000000, 0.000000000000000000, 0.000000000000000000 ) ) ;
#8804=EDGE_LOOP ( 'NONE', ( #4456, #6614, #22048, #8560 ) ) ;
#8812=CARTESIAN_POINT ( 'NONE',  ( -4.154094228333456762, 2.398367420968013253, -3.721909803043220055 ) ) ;
#8852=EDGE_CURVE ( 'NONE', #7786, #1506, #12671, .T. ) ;
#8853=ORIENTED_EDGE ( 'NONE', *, *, #19222, .T. ) ;
#8875=CARTESIAN_POINT ( 'NONE',  ( 1.567478505476135000E-15, 4.618802153517012954, -3.504269196027527844 ) ) ;
#8898=CARTESIAN_POINT ( 'NONE',  ( -2.712762565639006418, 3.052587955997511759, -3.430618716626627318 ) ) ;
#8914=ORIENTED_EDGE ( 'NONE', *, *, #10570, .F. ) ;
#8936=ADVANCED_FACE ( 'NONE', ( #1540 ), #23630, .F. ) ;
#8984=CARTESIAN_POINT ( 'NONE',  ( 2.548804901056335857E-15, 4.736522675502163437, -3.681124513963624612 ) ) ;
#8994=CARTESIAN_POINT ( 'NONE',  ( 4.211399257449709665, -2.459727064652517114, -3.751161691472417736 ) ) ;
#9015=DIRECTION ( 'NONE',  ( -0.000000000000000000, -0.000000000000000000, 1.000000000000000000 ) ) ;
#9048=CARTESIAN_POINT ( 'NONE',  ( -4.000000000000000000, 2.309401076758498483, -3.433295621305379353 ) ) ;
#9052=CIRCLE ( 'NONE', #15214, 2.500000000000000888 ) ;
#9072=CARTESIAN_POINT ( 'NONE',  ( -4.235886605889389145, -2.417314728048544303, -3.751161874094020909 ) ) ;
#9098=CARTESIAN_POINT ( 'NONE',  ( -3.974344831685191280E-13, 4.796734841935104576, -3.721909803043223608 ) ) ;
#9110=CARTESIAN_POINT ( 'NONE',  ( 4.211405965630455661, 2.460463115436283932, -3.751298928144577882 ) ) ;
#9123=PLANE ( 'NONE',  #4170 ) ;
#9132=CARTESIAN_POINT ( 'NONE',  ( 4.000000000000000000, -2.309401076758514915, -3.433295621305383349 ) ) ;
#9137=ADVANCED_FACE ( 'NONE', ( #10227 ), #9178, .F. ) ;
#9159=CARTESIAN_POINT ( 'NONE',  ( -4.000000000000000000, 0.7924765000094600165, -0.05906175389889745803 ) ) ;
#9168=EDGE_LOOP ( 'NONE', ( #17567, #6787 ) ) ;
#9178=CONICAL_SURFACE ( 'NONE', #2610, 2.500000000000000888, 0.9599310885968785900 ) ;
#9187=EDGE_CURVE ( 'NONE', #1352, #7786, #13074, .T. ) ;
#9193=CARTESIAN_POINT ( 'NONE',  ( -4.140404888673278272, -2.228338276487456415, -3.686887068327035166 ) ) ;
#9231=ORIENTED_EDGE ( 'NONE', *, *, #7363, .T. ) ;
#9250=DIRECTION ( 'NONE',  ( -0.000000000000000000, -0.000000000000000000, 1.000000000000000000 ) ) ;
#9269=CARTESIAN_POINT ( 'NONE',  ( 4.000000000000000000, 2.309401076758515803, -0.4999999999999995559 ) ) ;
#9271=CARTESIAN_POINT ( 'NONE',  ( 4.024499207728657879, 2.323545700935571556, -3.572172305156506411 ) ) ;
#9359=EDGE_LOOP ( 'NONE', ( #561, #552, #20094, #7393 ) ) ;
#9386=EDGE_CURVE ( 'NONE', #15759, #17675, #16509, .T. ) ;
#9410=CARTESIAN_POINT ( 'NONE',  ( 4.000000000000000000, -1.560351142792952617, -0.2242961665059816367 ) ) ;
#9412=AXIS2_PLACEMENT_3D ( 'NONE', #4945, #16302, #5298 ) ;
#9437=CARTESIAN_POINT ( 'NONE',  ( 3.680118525130245732, -2.494084732383344605, -0.3507732604232533524 ) ) ;
#9463=AXIS2_PLACEMENT_3D ( 'NONE', #22173, #20245, #17977 ) ;
#9469=CARTESIAN_POINT ( 'NONE',  ( 4.204115023516791005, -1.660442669500199919, -3.602151381774560068 ) ) ;
#9473=CARTESIAN_POINT ( 'NONE',  ( 0.000000000000000000, 0.000000000000000000, 0.000000000000000000 ) ) ;
#9481=DIRECTION ( 'NONE',  ( -0.000000000000000000, 0.000000000000000000, -1.000000000000000000 ) ) ;
#9508=VERTEX_POINT ( 'NONE', #22739 ) ;
#9541=ORIENTED_EDGE ( 'NONE', *, *, #14479, .T. ) ;
#9553=CARTESIAN_POINT ( 'NONE',  ( 2.855764796983346177, -2.970025579236428737, -0.09382832055446485575 ) ) ;
#9596=AXIS2_PLACEMENT_3D ( 'NONE', #23047, #4829, #1076 ) ;
#9606=VERTEX_POINT ( 'NONE', #11794 ) ;
#9623=DIRECTION ( 'NONE',  ( -1.000000000000000000, 0.000000000000000000, 0.000000000000000000 ) ) ;
#9632=FILL_AREA_STYLE_COLOUR ( '', #20393 ) ;
#9651=CARTESIAN_POINT ( 'NONE',  ( 0.000000000000000000, 0.000000000000000000, -4.000000000000000000 ) ) ;
#9694=DIRECTION ( 'NONE',  ( -1.000000000000000000, 0.000000000000000000, 0.000000000000000000 ) ) ;
#9762=EDGE_CURVE ( 'NONE', #7620, #3485, #762, .T. ) ;
#9772=AXIS2_PLACEMENT_3D ( 'NONE', #23262, #1290, #1181 ) ;
#9781=EDGE_CURVE ( 'NONE', #14870, #6737, #1703, .T. ) ;
#9795=CARTESIAN_POINT ( 'NONE',  ( 4.203833317240879275, 1.627343821129582979, -3.597273115243889929 ) ) ;
#9822=( NAMED_UNIT ( * ) SI_UNIT ( $, .STERADIAN. ) SOLID_ANGLE_UNIT ( ) );
#9832=AXIS2_PLACEMENT_3D ( 'NONE', #17220, #2590, #13641 ) ;
#9864=PLANE ( 'NONE',  #9832 ) ;
#9881=CARTESIAN_POINT ( 'NONE',  ( -3.679171394226034675, -2.494631558665844739, -0.3503314178412558211 ) ) ;
#9918=CARTESIAN_POINT ( 'NONE',  ( 4.175002511812151873, 2.208363329454889445, -3.469254087858244073 ) ) ;
#9950=CONICAL_SURFACE ( 'NONE', #18394, 2.500000000000000888, 0.9599310885968785900 ) ;
#9960=DIRECTION ( 'NONE',  ( -1.000000000000000000, 0.000000000000000000, 0.000000000000000000 ) ) ;
#10052=CARTESIAN_POINT ( 'NONE',  ( 4.197393957002303999, 7.772902908466098641E-14, -3.503767560748929810 ) ) ;
#10054=CIRCLE ( 'NONE', #23527, 2.100000000000000089 ) ;
#10113=CARTESIAN_POINT ( 'NONE',  ( -4.000000000000000000, 0.000000000000000000, 0.000000000000000000 ) ) ;
#10152=CONICAL_SURFACE ( 'NONE', #9772, 4.000000000000000000, 0.8911886515913786111 ) ;
#10164=ADVANCED_FACE ( 'NONE', ( #16747 ), #94, .T. ) ;
#10210=CARTESIAN_POINT ( 'NONE',  ( 0.000000000000000000, 0.000000000000000000, -25.03750572909317285 ) ) ;
#10220=CARTESIAN_POINT ( 'NONE',  ( -3.510273485745307287, -2.827716139362669967, -3.610536846335890004 ) ) ;
#10225=SURFACE_SIDE_STYLE ('',( #12607 ) ) ;
#10227=FACE_OUTER_BOUND ( 'NONE', #13103, .T. ) ;
#10229=EDGE_LOOP ( 'NONE', ( #9231, #20878, #2000 ) ) ;
#10241=CARTESIAN_POINT ( 'NONE',  ( -2.855764796983342624, 2.970025579236414082, -0.09382832055445475272 ) ) ;
#10290=ORIENTED_EDGE ( 'NONE', *, *, #21312, .F. ) ;
#10330=CARTESIAN_POINT ( 'NONE',  ( -0.5449313310646672903, -4.304185902836978883, -3.316620875263469159 ) ) ;
#10360=DIRECTION ( 'NONE',  ( -0.000000000000000000, -0.000000000000000000, 1.000000000000000000 ) ) ;
#10369=VERTEX_POINT ( 'NONE', #17694 ) ;
#10481=EDGE_LOOP ( 'NONE', ( #17946, #14753, #23032 ) ) ;
#10519=ORIENTED_EDGE ( 'NONE', *, *, #22597, .F. ) ;
#10525=EDGE_CURVE ( 'NONE', #21860, #10369, #13539, .T. ) ;
#10552=DIRECTION ( 'NONE',  ( 0.9396926207859138680, 1.150791560227856926E-16, -0.3420201433256536139 ) ) ;
#10570=EDGE_CURVE ( 'NONE', #20887, #13282, #14285, .T. ) ;
#10596=CARTESIAN_POINT ( 'NONE',  ( 0.1404048886732821022, 4.699864953788070565, -3.686887068327037387 ) ) ;
#10625=VERTEX_POINT ( 'NONE', #14921 ) ;
#10628=ORIENTED_EDGE ( 'NONE', *, *, #22635, .F. ) ;
#10672=EDGE_CURVE ( 'NONE', #18124, #160, #21960, .T. ) ;
#10705=DIRECTION ( 'NONE',  ( -0.5000000000000016653, 0.8660254037844378194, 0.000000000000000000 ) ) ;
#10727=CARTESIAN_POINT ( 'NONE',  ( 1.999999999999998224, -3.464101615137772594, -3.142992957459239012 ) ) ;
#10759=DIRECTION ( 'NONE',  ( 1.000000000000000000, 0.000000000000000000, 0.000000000000000000 ) ) ;
#10810=CONICAL_SURFACE ( 'NONE', #15037, 2.059999999999998721, 0.9599310885968738161 ) ;
#10823=CARTESIAN_POINT ( 'NONE',  ( 1.411581201560190495E-15, 4.862606272033091592, -3.745885042887436622 ) ) ;
#10862=CARTESIAN_POINT ( 'NONE',  ( -4.000000000000000000, -7.806255641895631925E-15, -3.142992957459232350 ) ) ;
#10899=LINE ( 'NONE', #21961, #8214 ) ;
#10926=CARTESIAN_POINT ( 'NONE',  ( 4.000000000000000000, 0.7924765000094659007, -0.05906175389889852662 ) ) ;
#10952=DIRECTION ( 'NONE',  ( 0.000000000000000000, 0.000000000000000000, -1.000000000000000000 ) ) ;
#10956=EDGE_LOOP ( 'NONE', ( #22582, #2774, #688, #1092 ) ) ;
#11005=FACE_OUTER_BOUND ( 'NONE', #12267, .T. ) ;
#11011=CARTESIAN_POINT ( 'NONE',  ( 3.999999999999999112, -0.7890432684750902093, -0.04868663549882291247 ) ) ;
#11026=CARTESIAN_POINT ( 'NONE',  ( 0.02511973781850649831, -4.877415612947427981, -3.751298745799844792 ) ) ;
#11059=CARTESIAN_POINT ( 'NONE',  ( 4.000000000000000000, 1.680228229147133767, -3.316631783032546021 ) ) ;
#11089=CARTESIAN_POINT ( 'NONE',  ( -5.560781378645575757, 6.809993116116508640E-16, -4.000000000000000000 ) ) ;
#11096=CARTESIAN_POINT ( 'NONE',  ( 0.3208286057739604957, -4.433571671609698228, -0.3503314178412692548 ) ) ;
#11107=CARTESIAN_POINT ( 'NONE',  ( -3.333333333333335258, 2.694301256218251783, -3.300726591567079815 ) ) ;
#11187=CARTESIAN_POINT ( 'NONE',  ( 1.393927851585479161, -4.043713361053543842, -3.526374918436840922 ) ) ;
#11195=CIRCLE ( 'NONE', #5423, 5.384454397937118664 ) ;
#11201=ORIENTED_EDGE ( 'NONE', *, *, #1470, .T. ) ;
#11210=AXIS2_PLACEMENT_3D ( 'NONE', #9473, #14914, #3769 ) ;
#11215=ORIENTED_EDGE ( 'NONE', *, *, #19222, .F. ) ;
#11227=CARTESIAN_POINT ( 'NONE',  ( 4.101954839143060028, 2.368264730582927857, -3.681130640444267854 ) ) ;
#11231=CARTESIAN_POINT ( 'NONE',  ( 1.317756351988342622, -3.857995168970215438, -0.04852650426602527628 ) ) ;
#11235=EDGE_LOOP ( 'NONE', ( #16347, #11390, #1675, #15506, #20604, #21898 ) ) ;
#11250=CARTESIAN_POINT ( 'NONE',  ( -6.259644161404860030E-16, -4.618802153517027165, -3.433295621305388234 ) ) ;
#11257=CARTESIAN_POINT ( 'NONE',  ( 0.6666666666666689611, 4.233901974057261874, -3.300726591567082480 ) ) ;
#11262=ADVANCED_FACE ( 'NONE', ( #15758 ), #5729, .F. ) ;
#11305=CARTESIAN_POINT ( 'NONE',  ( -0.3461262719736137305, 4.658553426539289610, -3.671615880910373608 ) ) ;
#11307=CARTESIAN_POINT ( 'NONE',  ( 1.747541505913279281, -3.837784562140273081, -3.503702292528912299 ) ) ;
#11348=CARTESIAN_POINT ( 'NONE',  ( -4.000000000000000000, 2.309401076758498483, -0.4999999999999927280 ) ) ;
#11353=CARTESIAN_POINT ( 'NONE',  ( -1.240299975428134203E-15, -4.736529461165891242, -3.681130640444276292 ) ) ;
#11390=ORIENTED_EDGE ( 'NONE', *, *, #15368, .F. ) ;
#11407=CONICAL_SURFACE ( 'NONE', #5984, 4.000000000000000000, 0.8911886515913786111 ) ;
#11437=VERTEX_POINT ( 'NONE', #22449 ) ;
#11445=ORIENTED_EDGE ( 'NONE', *, *, #14744, .T. ) ;
#11448=CARTESIAN_POINT ( 'NONE',  ( 0.000000000000000000, 0.000000000000000000, 0.000000000000000000 ) ) ;
#11525=ORIENTED_EDGE ( 'NONE', *, *, #18781, .F. ) ;
#11528=( NAMED_UNIT ( * ) PLANE_ANGLE_UNIT ( ) SI_UNIT ( $, .RADIAN. ) );
#11580=ADVANCED_FACE ( 'NONE', ( #11750 ), #23172, .F. ) ;
#11589=ORIENTED_EDGE ( 'NONE', *, *, #5427, .T. ) ;
#11686=ADVANCED_FACE ( 'NONE', ( #7215 ), #2445, .T. ) ;
#11698=CARTESIAN_POINT ( 'NONE',  ( -1.312671235360383548, -3.860931062424228788, -0.05923475698271369466 ) ) ;
#11703=CARTESIAN_POINT ( 'NONE',  ( -4.211140560182196957, -2.431303136016552013, -3.745885042887436178 ) ) ;
#11709=VECTOR ( 'NONE', #8192, 1000.000000000000000 ) ;
#11721=CARTESIAN_POINT ( 'NONE',  ( 4.211140560182196957, -2.431303136016555122, -3.745885042887436622 ) ) ;
#11724=B_SPLINE_CURVE_WITH_KNOTS ( 'NONE', 3,
 ( #6253, #21090, #13659, #10241, #17119, #12090, #4546, #17582 ),
 .UNSPECIFIED., .F., .F.,
 ( 4, 2, 2, 4 ),
 ( 2.465131517071352357E-07, 0.001183067374689843057, 0.001774477805458910071, 0.002365888236227977302 ),
 .UNSPECIFIED. ) ;
#11732=EDGE_CURVE ( 'NONE', #5401, #20231, #16212, .T. ) ;
#11750=FACE_OUTER_BOUND ( 'NONE', #19172, .T. ) ;
#11766=CARTESIAN_POINT ( 'NONE',  ( 3.510273485745307731, 2.827716139362654424, -3.610536846335885564 ) ) ;
#11794=CARTESIAN_POINT ( 'NONE',  ( 4.000000000000000000, -2.309401076758514915, -3.433295621305383349 ) ) ;
#11822=CARTESIAN_POINT ( 'NONE',  ( -0.6920835326022555245, -4.454600218803899558, -3.597382984111586079 ) ) ;
#11843=CARTESIAN_POINT ( 'NONE',  ( 4.198928548860774157, -0.8158838809860124996, -3.526471437616918170 ) ) ;
#11873=CARTESIAN_POINT ( 'NONE',  ( 0.000000000000000000, 0.000000000000000000, -25.03750572909317285 ) ) ;
#11877=CARTESIAN_POINT ( 'NONE',  ( 2.756197834950227410, 3.027510591568626896, -3.223146290109805356 ) ) ;
#11892=EDGE_CURVE ( 'NONE', #21528, #13636, #19790, .T. ) ;
#11992=AXIS2_PLACEMENT_3D ( 'NONE', #9651, #13409, #464 ) ;
#12005=DIRECTION ( 'NONE',  ( 1.000000000000000000, 0.000000000000000000, 0.000000000000000000 ) ) ;
#12008=CARTESIAN_POINT ( 'NONE',  ( 4.235886605889389145, 2.417314728048528760, -3.751161874094018245 ) ) ;
#12012=CARTESIAN_POINT ( 'NONE',  ( 3.522875095019493141, -2.820352903225631369, -3.598441714920572299 ) ) ;
#12035=EDGE_CURVE ( 'NONE', #4834, #6737, #9052, .T. ) ;
#12066=DIRECTION ( 'NONE',  ( -0.000000000000000000, -0.000000000000000000, 1.000000000000000000 ) ) ;
#12082=CARTESIAN_POINT ( 'NONE',  ( -4.211399284164270895, 2.459729995988205964, -3.751162237960538715 ) ) ;
#12090=CARTESIAN_POINT ( 'NONE',  ( -2.345747346278108214, 3.264484291692489215, -0.01223254789873409049 ) ) ;
#12107=VERTEX_POINT ( 'NONE', #22039 ) ;
#12170=CARTESIAN_POINT ( 'NONE',  ( 0.1756481739660539498, -4.720212674038995360, -3.469390959564070620 ) ) ;
#12247=ORIENTED_EDGE ( 'NONE', *, *, #18419, .F. ) ;
#12250=CARTESIAN_POINT ( 'NONE',  ( -2.000000000000006661, 3.464101615137750834, 0.000000000000000000 ) ) ;
#12267=EDGE_LOOP ( 'NONE', ( #8853, #14541, #16683, #13804, #262, #5647, #2700 ) ) ;
#12271=CARTESIAN_POINT ( 'NONE',  ( 4.000000000000000000, 0.1981133338132474442, 2.382280164152719704E-17 ) ) ;
#12369=AXIS2_PLACEMENT_3D ( 'NONE', #18987, #9481, #16835 ) ;
#12428=CARTESIAN_POINT ( 'NONE',  ( 5.560781378645575757, 0.000000000000000000, -4.000000000000000000 ) ) ;
#12496=ORIENTED_EDGE ( 'NONE', *, *, #14908, .T. ) ;
#12526=VERTEX_POINT ( 'NONE', #18972 ) ;
#12530=ORIENTED_EDGE ( 'NONE', *, *, #17596, .T. ) ;
#12536=CIRCLE ( 'NONE', #21366, 2.499999999999999556 ) ;
#12544=CARTESIAN_POINT ( 'NONE',  ( -1.257172072275743346, 3.892973519171203378, -3.433252694550776862 ) ) ;
#12607=SURFACE_STYLE_FILL_AREA ( #7805 ) ;
#12639=ORIENTED_EDGE ( 'NONE', *, *, #7030, .T. ) ;
#12671=B_SPLINE_CURVE_WITH_KNOTS ( 'NONE', 3,
 ( #16636, #7328, #11231, #14715, #11096, #91 ),
 .UNSPECIFIED., .F., .F.,
 ( 4, 2, 4 ),
 ( 0.002365888236227967761, 0.003551327329835077609, 0.004736766423442186590 ),
 .UNSPECIFIED. ) ;
#12697=AXIS2_PLACEMENT_3D ( 'NONE', #13756, #19372, #21078 ) ;
#12716=DIRECTION ( 'NONE',  ( -0.8191520442889875797, 1.003171929053519570E-16, 0.5735764363510522656 ) ) ;
#12747=CARTESIAN_POINT ( 'NONE',  ( -2.500000000000000888, 0.000000000000000000, -4.974599999999998801 ) ) ;
#12794=CARTESIAN_POINT ( 'NONE',  ( -0.6640947660597427138, 4.471078309994878985, -3.602146406945963442 ) ) ;
#12814=CARTESIAN_POINT ( 'NONE',  ( 0.000000000000000000, 0.000000000000000000, 3.469446951953614189E-15 ) ) ;
#12834=CARTESIAN_POINT ( 'NONE',  ( -4.211140560182196957, 2.431303136016537803, -3.745885042887433514 ) ) ;
#12858=EDGE_CURVE ( 'NONE', #3485, #7620, #12536, .T. ) ;
#13021=EDGE_CURVE ( 'NONE', #160, #17167, #8510, .T. ) ;
#13034=DIRECTION ( 'NONE',  ( 0.000000000000000000, 0.000000000000000000, -1.000000000000000000 ) ) ;
#13037=EDGE_CURVE ( 'NONE', #14870, #15759, #15070, .T. ) ;
#13074=CIRCLE ( 'NONE', #12697, 4.000000000000000000 ) ;
#13103=EDGE_LOOP ( 'NONE', ( #19030, #22049, #2030, #2379 ) ) ;
#13129=CARTESIAN_POINT ( 'NONE',  ( 4.197310751797292738, 0.8178363989516252985, -3.502498386812444409 ) ) ;
#13182=ADVANCED_FACE ( 'NONE', ( #6341 ), #9864, .T. ) ;
#13200=FACE_OUTER_BOUND ( 'NONE', #9359, .T. ) ;
#13245=CARTESIAN_POINT ( 'NONE',  ( -1.393927851585477606, 4.043713361053528743, -3.526374918436835149 ) ) ;
#13246=CARTESIAN_POINT ( 'NONE',  ( 4.000000000000000000, 2.309401076758497151, -5.000000000000000000 ) ) ;
#13247=B_SPLINE_CURVE_WITH_KNOTS ( 'NONE', 3,
 ( #16624, #3555, #10727, #76, #9132 ),
 .UNSPECIFIED., .F., .F.,
 ( 4, 1, 4 ),
 ( 5.640274452250024914E-20, 0.002309401076758505356, 0.004618802153517010713 ),
 .UNSPECIFIED. ) ;
#13272=DIRECTION ( 'NONE',  ( 0.000000000000000000, 0.000000000000000000, 1.000000000000000000 ) ) ;
#13282=VERTEX_POINT ( 'NONE', #12428 ) ;
#13298=ORIENTED_EDGE ( 'NONE', *, *, #22597, .T. ) ;
#13330=DIRECTION ( 'NONE',  ( 0.000000000000000000, 0.000000000000000000, 1.000000000000000000 ) ) ;
#13337=VERTEX_POINT ( 'NONE', #1261 ) ;
#13354=EDGE_LOOP ( 'NONE', ( #126, #739, #15782 ) ) ;
#13356=CARTESIAN_POINT ( 'NONE',  ( -2.805705207896067144, 3.226868319750155312, -3.503898532754364581 ) ) ;
#13359=DIRECTION ( 'NONE',  ( 0.000000000000000000, 0.000000000000000000, -1.000000000000000000 ) ) ;
#13365=ORIENTED_EDGE ( 'NONE', *, *, #18670, .F. ) ;
#13374=VECTOR ( 'NONE', #18162, 1000.000000000000000 ) ;
#13409=DIRECTION ( 'NONE',  ( -0.000000000000000000, -0.000000000000000000, 1.000000000000000000 ) ) ;
#13464=ADVANCED_FACE ( 'NONE', ( #2328 ), #3795, .T. ) ;
#13486=ORIENTED_EDGE ( 'NONE', *, *, #7396, .T. ) ;
#13511=ORIENTED_EDGE ( 'NONE', *, *, #9781, .T. ) ;
#13515=( GEOMETRIC_REPRESENTATION_CONTEXT ( 3 ) GLOBAL_UNCERTAINTY_ASSIGNED_CONTEXT ( ( #20264 ) ) GLOBAL_UNIT_ASSIGNED_CONTEXT ( ( #18227, #21841, #23554 ) ) REPRESENTATION_CONTEXT ( 'NONE', 'WORKASPACE' ) );
#13534=VERTEX_POINT ( 'NONE', #757 ) ;
#13539=CIRCLE ( 'NONE', #19652, 2.500000000000000444 ) ;
#13558=CARTESIAN_POINT ( 'NONE',  ( 0.000000000000000000, 0.000000000000000000, -4.974599999999998801 ) ) ;
#13614=ORIENTED_EDGE ( 'NONE', *, *, #18745, .F. ) ;
#13636=VERTEX_POINT ( 'NONE', #4267 ) ;
#13641=DIRECTION ( 'NONE',  ( -0.8660254037844373753, 0.5000000000000021094, 0.000000000000000000 ) ) ;
#13659=CARTESIAN_POINT ( 'NONE',  ( -3.355112389629170799, 2.681727112203152963, -0.2256878752776689534 ) ) ;
#13686=CARTESIAN_POINT ( 'NONE',  ( -4.024497503033519941, -2.323544716729390558, -3.572167766733381544 ) ) ;
#13690=CARTESIAN_POINT ( 'NONE',  ( 4.211140560182196957, 2.431303136016536470, -3.745885042887433514 ) ) ;
#13702=CARTESIAN_POINT ( 'NONE',  ( 2.449848172108560096, 3.432307619358740514, -3.503702292528905637 ) ) ;
#13756=CARTESIAN_POINT ( 'NONE',  ( 0.000000000000000000, 0.000000000000000000, 0.000000000000000000 ) ) ;
#13757=CARTESIAN_POINT ( 'NONE',  ( -3.999999999998910649, -1.658469974638591804, -3.531532913075256186 ) ) ;
#13782=FACE_OUTER_BOUND ( 'NONE', #13354, .T. ) ;
#13804=ORIENTED_EDGE ( 'NONE', *, *, #20695, .F. ) ;
#13807=CARTESIAN_POINT ( 'NONE',  ( 2.807080416178989513, -3.225969019225150003, -3.502507215260505014 ) ) ;
#13822=EDGE_CURVE ( 'NONE', #12, #7786, #3264, .T. ) ;
#13866=PRODUCT ( 'hex flange nut gradea_iso_ISO - 4161 - M5 - N', 'hex flange nut gradea_iso_ISO - 4161 - M5 - N', '', ( #226 ) ) ;
#13871=CARTESIAN_POINT ( 'NONE',  ( -3.861362476283256129, -2.629030857716004199, -3.671615880910374941 ) ) ;
#13888=STYLED_ITEM('',(#23927),#4039);
#13935=CARTESIAN_POINT ( 'NONE',  ( -0.1750025118121544265, -4.719839900820635314, -3.469254087858253399 ) ) ;
#13949=AXIS2_PLACEMENT_3D ( 'NONE', #4386, #20926, #9960 ) ;
#13967=ORIENTED_EDGE ( 'NONE', *, *, #1635, .F. ) ;
#13981=CARTESIAN_POINT ( 'NONE',  ( -0.6810597143197697489, -4.461075778259609770, -3.598441714920717516 ) ) ;
#14022=ADVANCED_FACE ( 'NONE', ( #20897 ), #2659, .T. ) ;
#14025=EDGE_LOOP ( 'NONE', ( #11445, #8385, #20754, #7670 ) ) ;
#14039=CARTESIAN_POINT ( 'NONE',  ( 1.257172072275274388, -3.892973519170983110, -3.433252694550781303 ) ) ;
#14092=EDGE_CURVE ( 'NONE', #17675, #3485, #1771, .T. ) ;
#14118=CARTESIAN_POINT ( 'NONE',  ( -4.000000000000000000, -2.309401076758512694, -3.433295621305382461 ) ) ;
#14129=CARTESIAN_POINT ( 'NONE',  ( -2.499999999999999556, 3.061616997868382648E-16, 3.469446951953614189E-15 ) ) ;
#14136=ORIENTED_EDGE ( 'NONE', *, *, #18714, .F. ) ;
#14138=CARTESIAN_POINT ( 'NONE',  ( 0.6920835326022565237, 4.454600218803884459, -3.597382984111579862 ) ) ;
#14156=CARTESIAN_POINT ( 'NONE',  ( 0.5469614295415388128, -4.303013824935362663, -3.535263753543555598 ) ) ;
#14160=ORIENTED_EDGE ( 'NONE', *, *, #20668, .F. ) ;
#14173=CARTESIAN_POINT ( 'NONE',  ( -1.317756351988340180, 3.857995168970202116, -0.04852650426601388955 ) ) ;
#14191=EDGE_CURVE ( 'NONE', #13282, #20887, #19253, .T. ) ;
#14220=CARTESIAN_POINT ( 'NONE',  ( -4.000000000000000000, -2.472261339043343220, -3.687027428081192326 ) ) ;
#14248=DIRECTION ( 'NONE',  ( -0.9396926207859138680, 0.000000000000000000, -0.3420201433256536139 ) ) ;
#14266=AXIS2_PLACEMENT_3D ( 'NONE', #16822, #13359, #20672 ) ;
#14285=CIRCLE ( 'NONE', #17344, 5.560781378645573980 ) ;
#14302=EDGE_LOOP ( 'NONE', ( #2872, #19664, #5281, #19400, #20540 ) ) ;
#14313=EDGE_CURVE ( 'NONE', #8518, #18124, #11724, .T. ) ;
#14345=CARTESIAN_POINT ( 'NONE',  ( 0.02448733951239481094, 4.877042772274728044, -3.751161874094022242 ) ) ;
#14382=DIRECTION ( 'NONE',  ( -1.000000000000000000, 0.000000000000000000, 0.000000000000000000 ) ) ;
#14406=EDGE_LOOP ( 'NONE', ( #19945, #1204, #13511, #7882 ) ) ;
#14429=CARTESIAN_POINT ( 'NONE',  ( 0.000000000000000000, 0.000000000000000000, -5.000000000000000000 ) ) ;
#14447=CARTESIAN_POINT ( 'NONE',  ( -3.522875095019672109, 2.820352903225427532, -3.598441714920591394 ) ) ;
#14474=DIRECTION ( 'NONE',  ( 1.000000000000000000, 0.000000000000000000, 0.000000000000000000 ) ) ;
#14479=EDGE_CURVE ( 'NONE', #4882, #19949, #3843, .T. ) ;
#14496=CLOSED_SHELL ( 'NONE', ( #11580, #9137, #6321, #19449, #8547, #8936, #5163, #22400, #13182, #7565, #10164, #18254, #14022, #16278, #22669, #6598, #16540, #17438, #18298, #13464, #6399, #7613, #11686, #11262, #5865, #15043, #22562, #15206, #19195, #15675, #21723, #19023 ) ) ;
#14516=ORIENTED_EDGE ( 'NONE', *, *, #23640, .F. ) ;
#14534=CARTESIAN_POINT ( 'NONE',  ( 4.000000000000000888, 1.563622288139206118, -0.2253451193528334950 ) ) ;
#14541=ORIENTED_EDGE ( 'NONE', *, *, #4099, .T. ) ;
#14546=DIRECTION ( 'NONE',  ( 0.000000000000000000, 0.000000000000000000, 1.000000000000000000 ) ) ;
#14562=FACE_OUTER_BOUND ( 'NONE', #11235, .T. ) ;
#14626=PRODUCT_DEFINITION_SHAPE ( 'NONE', 'NONE',  #16837 ) ;
#14635=CARTESIAN_POINT ( 'NONE',  ( -1.287237434361707233, -3.875615274277397937, -3.430618716626816500 ) ) ;
#14656=CARTESIAN_POINT ( 'NONE',  ( 4.000000000000000000, 2.309401076758515803, -0.4999999999999995559 ) ) ;
#14666=CARTESIAN_POINT ( 'NONE',  ( 1.567478505476134606E-15, 4.618802153517012066, -3.433295621305382905 ) ) ;
#14668=ORIENTED_EDGE ( 'NONE', *, *, #14908, .F. ) ;
#14691=CARTESIAN_POINT ( 'NONE',  ( 0.000000000000000000, 0.000000000000000000, -4.000000000000000000 ) ) ;
#14696=CIRCLE ( 'NONE', #13949, 4.000000000000000000 ) ;
#14702=CARTESIAN_POINT ( 'NONE',  ( -4.000000000000000888, -1.539600717839011201, -3.300726591567081591 ) ) ;
#14715=CARTESIAN_POINT ( 'NONE',  ( 0.6507732100473444525, -4.243078065514795050, -0.2236248678334952777 ) ) ;
#14723=CARTESIAN_POINT ( 'NONE',  ( -0.6666666666666651864, 4.233901974057260098, -3.300726591567081147 ) ) ;
#14726=CARTESIAN_POINT ( 'NONE',  ( -4.000000000000000888, 1.563622288139195238, -0.2253451193528307472 ) ) ;
#14744=EDGE_CURVE ( 'NONE', #17675, #15759, #10054, .T. ) ;
#14753=ORIENTED_EDGE ( 'NONE', *, *, #22250, .F. ) ;
#14766=ORIENTED_EDGE ( 'NONE', *, *, #23430, .F. ) ;
#14784=B_SPLINE_CURVE_WITH_KNOTS ( 'NONE', 3,
 ( #23004, #8652, #21443, #8298, #6718, #4906 ),
 .UNSPECIFIED., .F., .F.,
 ( 4, 2, 4 ),
 ( 4.336808689942017736E-19, 0.0002095117440854729585, 0.0004190234881709454834 ),
 .UNSPECIFIED. ) ;
#14791=CARTESIAN_POINT ( 'NONE',  ( 4.000000000000000000, -1.677850389431204459, -3.535268758346977513 ) ) ;
#14825=CARTESIAN_POINT ( 'NONE',  ( -4.000000000000000000, 0.000000000000000000, 0.000000000000000000 ) ) ;
#14857=VECTOR ( 'NONE', #10552, 1000.000000000000227 ) ;
#14870=VERTEX_POINT ( 'NONE', #20479 ) ;
#14879=CARTESIAN_POINT ( 'NONE',  ( 2.000000000000005329, -3.464101615137751722, 0.000000000000000000 ) ) ;
#14896=EDGE_CURVE ( 'NONE', #21860, #4834, #6241, .T. ) ;
#14899=DIRECTION ( 'NONE',  ( -0.000000000000000000, -0.000000000000000000, 1.000000000000000000 ) ) ;
#14902=ORIENTED_EDGE ( 'NONE', *, *, #17601, .T. ) ;
#14904=CARTESIAN_POINT ( 'NONE',  ( -2.500000000000000444, 3.061616997868383634E-16, -25.03750572909317285 ) ) ;
#14908=EDGE_CURVE ( 'NONE', #18021, #11437, #15190, .T. ) ;
#14912=CARTESIAN_POINT ( 'NONE',  ( -4.197393957002303999, 0.4069871074557429025, -3.503767560748926257 ) ) ;
#14914=DIRECTION ( 'NONE',  ( 0.000000000000000000, 0.000000000000000000, 1.000000000000000000 ) ) ;
#14921=CARTESIAN_POINT ( 'NONE',  ( -4.197393957002303999, -7.773935952363655451E-14, -3.503767560748929810 ) ) ;
#15037=AXIS2_PLACEMENT_3D ( 'NONE', #16279, #23622, #3327 ) ;
#15043=ADVANCED_FACE ( 'NONE', ( #18907 ), #2186, .F. ) ;
#15057=ORIENTED_EDGE ( 'NONE', *, *, #11732, .T. ) ;
#15070=LINE ( 'NONE', #5863, #20573 ) ;
#15077=DIRECTION ( 'NONE',  ( -0.000000000000000000, -0.000000000000000000, 1.000000000000000000 ) ) ;
#15129=CARTESIAN_POINT ( 'NONE',  ( 3.355112389629172576, -2.681727112203168950, -0.2256878752776777242 ) ) ;
#15132=CARTESIAN_POINT ( 'NONE',  ( -4.211140560182196957, -2.431303136016552013, -3.745885042887436178 ) ) ;
#15161=CARTESIAN_POINT ( 'NONE',  ( 0.000000000000000000, 0.000000000000000000, -4.000000000000000000 ) ) ;
#15180=DIRECTION ( 'NONE',  ( 0.000000000000000000, 0.000000000000000000, 1.000000000000000000 ) ) ;
#15190=LINE ( 'NONE', #4173, #3861 ) ;
#15196=AXIS2_PLACEMENT_3D ( 'NONE', #11873, #19536, #12005 ) ;
#15201=CARTESIAN_POINT ( 'NONE',  ( 2.059999999999998721, 0.000000000000000000, -0.3080913168122742518 ) ) ;
#15204=CARTESIAN_POINT ( 'NONE',  ( 4.204015924366189871, -1.626724848190933548, -3.610627190413393084 ) ) ;
#15206=ADVANCED_FACE ( 'NONE', ( #5252 ), #520, .F. ) ;
#15214=AXIS2_PLACEMENT_3D ( 'NONE', #7181, #1281, #8659 ) ;
#15240=CARTESIAN_POINT ( 'NONE',  ( -4.000000000000000000, -2.309401076758512694, -5.000000000000000000 ) ) ;
#15269=FACE_BOUND ( 'NONE', #8534, .T. ) ;
#15280=CIRCLE ( 'NONE', #17197, 2.100000000000000089 ) ;
#15308=SHAPE_REPRESENTATION_RELATIONSHIP ( 'NONE' , 'NONE' ,  #5587, #6714 ) ;
#15357=DIRECTION ( 'NONE',  ( 0.000000000000000000, 0.000000000000000000, 1.000000000000000000 ) ) ;
#15366=CARTESIAN_POINT ( 'NONE',  ( -2.100000000000000089, 2.571758278209441957E-16, -0.2800830152838844622 ) ) ;
#15368=EDGE_CURVE ( 'NONE', #23662, #21209, #14696, .T. ) ;
#15405=DIRECTION ( 'NONE',  ( 0.000000000000000000, -0.000000000000000000, 1.000000000000000000 ) ) ;
#15427=LINE ( 'NONE', #8172, #20730 ) ;
#15443=CONICAL_SURFACE ( 'NONE', #6555, 5.560781378645573980, 1.221730476396046816 ) ;
#15484=CARTESIAN_POINT ( 'NONE',  ( 1.274258131564866448, 3.883108878240963513, -3.220599429844046568 ) ) ;
#15494=B_SPLINE_CURVE_WITH_KNOTS ( 'NONE', 3,
 ( #8502, #12271, #19574, #10926, #23800, #14534, #20174, #14656 ),
 .UNSPECIFIED., .F., .F.,
 ( 4, 2, 2, 4 ),
 ( 0.005725059856848645212, 0.006314084072593634418, 0.006903108288338624492, 0.008081156719828603771 ),
 .UNSPECIFIED. ) ;
#15506=ORIENTED_EDGE ( 'NONE', *, *, #9187, .F. ) ;
#15510=EDGE_CURVE ( 'NONE', #1352, #17167, #15494, .T. ) ;
#15554=CARTESIAN_POINT ( 'NONE',  ( -4.203934362469166963, -1.640673743454851286, -3.598432614606932756 ) ) ;
#15568=CARTESIAN_POINT ( 'NONE',  ( -0.6666666666666666297, -4.233901974057276973, -3.300726591567087365 ) ) ;
#15571=CIRCLE ( 'NONE', #18607, 4.000000000000000000 ) ;
#15599=FACE_OUTER_BOUND ( 'NONE', #3989, .T. ) ;
#15654=CARTESIAN_POINT ( 'NONE',  ( -1.654252653721913102, -3.663718938583024443, -0.01223254789874440342 ) ) ;
#15662=( NAMED_UNIT ( * ) SI_UNIT ( $, .STERADIAN. ) SOLID_ANGLE_UNIT ( ) );
#15675=ADVANCED_FACE ( 'NONE', ( #22222 ), #8026, .F. ) ;
#15705=CARTESIAN_POINT ( 'NONE',  ( -4.211140560182196957, -2.431303136016552013, -3.745885042887436178 ) ) ;
#15740=EDGE_LOOP ( 'NONE', ( #11525, #20697, #18980, #4899 ) ) ;
#15758=FACE_OUTER_BOUND ( 'NONE', #21278, .T. ) ;
#15759=VERTEX_POINT ( 'NONE', #15366 ) ;
#15773=EDGE_CURVE ( 'NONE', #9508, #12526, #17230, .T. ) ;
#15778=DIRECTION ( 'NONE',  ( -1.000000000000000000, 0.000000000000000000, 0.000000000000000000 ) ) ;
#15779=CARTESIAN_POINT ( 'NONE',  ( -4.000000000000000000, 0.8576368993457507139, -3.433240632782198709 ) ) ;
#15782=ORIENTED_EDGE ( 'NONE', *, *, #5427, .F. ) ;
#15789=STYLED_ITEM ( 'NONE', ( #6594 ), #6714 ) ;
#15798=CARTESIAN_POINT ( 'NONE',  ( -2.000000000000002665, -3.464101615137770374, -3.142992957459237680 ) ) ;
#15860=EDGE_LOOP ( 'NONE', ( #14160, #21204, #16794, #16131, #492 ) ) ;
#15862=CARTESIAN_POINT ( 'NONE',  ( 5.560781378645573980, 6.809993116116507654E-16, -4.000000000000000000 ) ) ;
#15949=CARTESIAN_POINT ( 'NONE',  ( 2.712762565639649015, -3.052587955997662306, -3.430618716626630871 ) ) ;
#15978=ORIENTED_EDGE ( 'NONE', *, *, #9386, .F. ) ;
#15998=CARTESIAN_POINT ( 'NONE',  ( -3.540020015735593439, -2.810662092924100630, -3.602146406945814672 ) ) ;
#16017=APPLICATION_CONTEXT ( 'automotive_design' ) ;
#16088=TOROIDAL_SURFACE ( 'NONE', #22233, 5.384454397937118664, 0.5155456020628804703 ) ;
#16129=CARTESIAN_POINT ( 'NONE',  ( -0.5276280594146446346, 4.314175951381965746, -3.320322319201721495 ) ) ;
#16131=ORIENTED_EDGE ( 'NONE', *, *, #13822, .T. ) ;
#16162=VERTEX_POINT ( 'NONE', #19495 ) ;
#16175=CARTESIAN_POINT ( 'NONE',  ( 0.000000000000000000, 0.000000000000000000, 0.000000000000000000 ) ) ;
#16212=B_SPLINE_CURVE_WITH_KNOTS ( 'NONE', 3,
 ( #12834, #8812, #3586, #19904, #8691, #9048 ),
 .UNSPECIFIED., .F., .F.,
 ( 4, 2, 4 ),
 ( -3.640115492410698714E-06, 0.0002066546034006521879, 0.0004169493222937151081 ),
 .UNSPECIFIED. ) ;
#16259=CARTESIAN_POINT ( 'NONE',  ( -2.807080416178626692, 3.225969019225154444, -3.502507215260441065 ) ) ;
#16262=CARTESIAN_POINT ( 'NONE',  ( 8.673617379884035472E-16, 4.618802153517012954, 0.000000000000000000 ) ) ;
#16278=ADVANCED_FACE ( 'NONE', ( #1732, #14562 ), #9123, .F. ) ;
#16279=CARTESIAN_POINT ( 'NONE',  ( 0.000000000000000000, 0.000000000000000000, -0.3080913168122742518 ) ) ;
#16294=ORIENTED_EDGE ( 'NONE', *, *, #11892, .F. ) ;
#16302=DIRECTION ( 'NONE',  ( 0.000000000000000000, 0.000000000000000000, -1.000000000000000000 ) ) ;
#16322=LINE ( 'NONE', #21851, #6355 ) ;
#16323=ORIENTED_EDGE ( 'NONE', *, *, #15368, .T. ) ;
#16347=ORIENTED_EDGE ( 'NONE', *, *, #21109, .F. ) ;
#16352=CARTESIAN_POINT ( 'NONE',  ( 2.805705207896068476, -3.226868319750173075, -3.503898532754370354 ) ) ;
#16377=DIRECTION ( 'NONE',  ( -1.000000000000000000, 0.000000000000000000, 0.000000000000000000 ) ) ;
#16434=CARTESIAN_POINT ( 'NONE',  ( -1.390230914382372118, -4.043987460488664532, -3.502507215260523665 ) ) ;
#16436=CARTESIAN_POINT ( 'NONE',  ( 0.3198814748697593746, 4.434118497892183264, -0.3507732604232499107 ) ) ;
#16446=CARTESIAN_POINT ( 'NONE',  ( -2.500000000000000888, 0.000000000000000000, -4.974599999999998801 ) ) ;
#16454=B_SPLINE_CURVE_WITH_KNOTS ( 'NONE', 3,
 ( #6727, #6842, #1283, #21453, #21229 ),
 .UNSPECIFIED., .F., .F.,
 ( 4, 1, 4 ),
 ( 0.000000000000000000, 0.002309401076758505790, 0.004618802153517011580 ),
 .UNSPECIFIED. ) ;
#16462=EDGE_LOOP ( 'NONE', ( #8486, #2961, #13298, #1305, #1944, #5956, #7781 ) ) ;
#16475=DIRECTION ( 'NONE',  ( -1.000000000000000000, 0.000000000000000000, 0.000000000000000000 ) ) ;
#16509=CIRCLE ( 'NONE', #19575, 2.100000000000000089 ) ;
#16540=ADVANCED_FACE ( 'NONE', ( #652 ), #3315, .T. ) ;
#16602=CARTESIAN_POINT ( 'NONE',  ( 4.211140560182196957, -2.431303136016555122, -3.745885042887436622 ) ) ;
#16614=DIRECTION ( 'NONE',  ( 1.000000000000000000, 0.000000000000000000, 0.000000000000000000 ) ) ;
#16624=CARTESIAN_POINT ( 'NONE',  ( -6.259644161404860030E-16, -4.618802153517027165, -3.433295621305388234 ) ) ;
#16632=CARTESIAN_POINT ( 'NONE',  ( -4.000000000000000000, -0.7890432684750890990, -0.04868663549882315533 ) ) ;
#16636=CARTESIAN_POINT ( 'NONE',  ( 2.000000000000005329, -3.464101615137751722, 0.000000000000000000 ) ) ;
#16646=CARTESIAN_POINT ( 'NONE',  ( -4.000000000000000000, 0.3987449864459974846, -0.01220643443059782861 ) ) ;
#16664=UNCERTAINTY_MEASURE_WITH_UNIT (LENGTH_MEASURE( 1.000000000000000082E-05 ), #20960, 'distance_accuracy_value', 'NONE');
#16683=ORIENTED_EDGE ( 'NONE', *, *, #14191, .T. ) ;
#16747=FACE_OUTER_BOUND ( 'NONE', #15860, .T. ) ;
#16794=ORIENTED_EDGE ( 'NONE', *, *, #4305, .T. ) ;
#16802=B_SPLINE_CURVE_WITH_KNOTS ( 'NONE', 3,
 ( #20844, #11822, #2592, #22986, #4529, #10220, #13871, #11703 ),
 .UNSPECIFIED., .F., .F.,
 ( 4, 2, 2, 4 ),
 ( 0.000000000000000000, 0.002450665683189818828, 0.003675998524784728459, 0.004901331366379638524 ),
 .UNSPECIFIED. ) ;
#16822=CARTESIAN_POINT ( 'NONE',  ( 0.000000000000000000, 0.000000000000000000, 0.000000000000000000 ) ) ;
#16835=DIRECTION ( 'NONE',  ( -1.000000000000000000, 0.000000000000000000, 0.000000000000000000 ) ) ;
#16837=PRODUCT_DEFINITION ( 'UNKNOWN', '', #20063, #2024 ) ;
#16849=CARTESIAN_POINT ( 'NONE',  ( -2.688821387764050996E-14, -4.618802153517012954, -0.4999999999999995559 ) ) ;
#16853=CARTESIAN_POINT ( 'NONE',  ( 4.000000000000000000, 2.309401076758497151, -3.433295621305379353 ) ) ;
#16885=B_SPLINE_CURVE_WITH_KNOTS ( 'NONE', 3,
 ( #23766, #7222, #9410, #11011, #21731, #18445 ),
 .UNSPECIFIED., .F., .F.,
 ( 4, 2, 4 ),
 ( 0.003358874760055551890, 0.004541967308452098118, 0.005725059856848645212 ),
 .UNSPECIFIED. ) ;
#16915=LINE ( 'NONE', #15240, #3548 ) ;
#16917=CARTESIAN_POINT ( 'NONE',  ( 2.345747346278113987, -3.264484291692503870, -0.01223254789874484924 ) ) ;
#16938=VECTOR ( 'NONE', #5880, 999.9999999999998863 ) ;
#17097=CARTESIAN_POINT ( 'NONE',  ( 3.349226789952652439, 2.685125164760731487, -0.2236248678334773199 ) ) ;
#17119=CARTESIAN_POINT ( 'NONE',  ( -2.687328764639638656, 3.067272167851286202, -0.05923475698270370959 ) ) ;
#17136=PLANE ( 'NONE',  #21405 ) ;
#17167=VERTEX_POINT ( 'NONE', #10 ) ;
#17185=CARTESIAN_POINT ( 'NONE',  ( -4.000000000000000000, 2.309401076758498483, -3.433295621305379353 ) ) ;
#17194=ORIENTED_EDGE ( 'NONE', *, *, #4599, .F. ) ;
#17197=AXIS2_PLACEMENT_3D ( 'NONE', #5265, #9015, #16377 ) ;
#17219=FACE_OUTER_BOUND ( 'NONE', #22471, .T. ) ;
#17220=CARTESIAN_POINT ( 'NONE',  ( 4.000000000000000000, 2.309401076758497151, -5.000000000000000000 ) ) ;
#17230=B_SPLINE_CURVE_WITH_KNOTS ( 'NONE', 3,
 ( #8680, #14138, #22823, #13702, #21468, #11766, #19076, #17736 ),
 .UNSPECIFIED., .F., .F.,
 ( 4, 2, 2, 4 ),
 ( 7.780516681398759253E-20, 0.002450665683189819696, 0.003675998524784729327, 0.004901331366379639391 ),
 .UNSPECIFIED. ) ;
#17251=DIRECTION ( 'NONE',  ( -0.000000000000000000, -0.000000000000000000, 1.000000000000000000 ) ) ;
#17252=AXIS2_PLACEMENT_3D ( 'NONE', #16175, #3476, #14382 ) ;
#17277=CARTESIAN_POINT ( 'NONE',  ( 1.828356344711641102, 3.563200125723180900, -5.433716356636336675E-16 ) ) ;
#17344=AXIS2_PLACEMENT_3D ( 'NONE', #14691, #9250, #16614 ) ;
#17346=( GEOMETRIC_REPRESENTATION_CONTEXT ( 3 ) GLOBAL_UNCERTAINTY_ASSIGNED_CONTEXT ( ( #20875 ) ) GLOBAL_UNIT_ASSIGNED_CONTEXT ( ( #20792, #11528, #9822 ) ) REPRESENTATION_CONTEXT ( 'NONE', 'WORKASPACE' ) );
#17402=CARTESIAN_POINT ( 'NONE',  ( 4.140404888673277384, 2.228338276487440428, -3.686887068327033390 ) ) ;
#17438=ADVANCED_FACE ( 'NONE', ( #1421 ), #3353, .T. ) ;
#17524=CARTESIAN_POINT ( 'NONE',  ( -0.6507732100473471171, 4.243078065514775510, -0.2236248678334823436 ) ) ;
#17553=ORIENTED_EDGE ( 'NONE', *, *, #17596, .F. ) ;
#17565=DIRECTION ( 'NONE',  ( -1.000000000000000000, 0.000000000000000000, 0.000000000000000000 ) ) ;
#17567=ORIENTED_EDGE ( 'NONE', *, *, #12858, .F. ) ;
#17582=CARTESIAN_POINT ( 'NONE',  ( -2.000000000000006661, 3.464101615137750834, 0.000000000000000000 ) ) ;
#17596=EDGE_CURVE ( 'NONE', #10369, #21860, #23034, .T. ) ;
#17601=EDGE_CURVE ( 'NONE', #18021, #20231, #1017, .T. ) ;
#17619=FACE_OUTER_BOUND ( 'NONE', #3885, .T. ) ;
#17675=VERTEX_POINT ( 'NONE', #18312 ) ;
#17694=CARTESIAN_POINT ( 'NONE',  ( -2.500000000000000444, 3.061616997868383634E-16, -5.000000000000000888 ) ) ;
#17736=CARTESIAN_POINT ( 'NONE',  ( 4.211140560182196957, 2.431303136016536470, -3.745885042887433514 ) ) ;
#17792=ORIENTED_EDGE ( 'NONE', *, *, #12035, .T. ) ;
#17812=DIRECTION ( 'NONE',  ( -0.8660254037844377084, -0.5000000000000015543, 0.000000000000000000 ) ) ;
#17889=CARTESIAN_POINT ( 'NONE',  ( 1.734723475976807094E-15, 4.618802153517012954, -0.4999999999999995559 ) ) ;
#17946=ORIENTED_EDGE ( 'NONE', *, *, #8013, .T. ) ;
#17977=DIRECTION ( 'NONE',  ( -1.000000000000000000, 1.224646799147352714E-16, 0.000000000000000000 ) ) ;
#18015=DIRECTION ( 'NONE',  ( 1.000000000000000000, 0.000000000000000000, 0.000000000000000000 ) ) ;
#18020=ORIENTED_EDGE ( 'NONE', *, *, #15510, .F. ) ;
#18021=VERTEX_POINT ( 'NONE', #20910 ) ;
#18023=DIRECTION ( 'NONE',  ( -0.000000000000000000, -0.000000000000000000, 1.000000000000000000 ) ) ;
#18034=AXIS2_PLACEMENT_3D ( 'NONE', #8025, #15405, #4144 ) ;
#18124=VERTEX_POINT ( 'NONE', #12250 ) ;
#18162=DIRECTION ( 'NONE',  ( -0.000000000000000000, -0.000000000000000000, 1.000000000000000000 ) ) ;
#18227=( LENGTH_UNIT ( ) NAMED_UNIT ( * ) SI_UNIT ( .MILLI., .METRE. ) );
#18254=ADVANCED_FACE ( 'NONE', ( #6268 ), #17136, .T. ) ;
#18298=ADVANCED_FACE ( 'NONE', ( #19168 ), #11407, .T. ) ;
#18308=DIRECTION ( 'NONE',  ( 0.5000000000000013323, -0.8660254037844379305, 0.000000000000000000 ) ) ;
#18312=CARTESIAN_POINT ( 'NONE',  ( 2.100000000000000089, 0.000000000000000000, -0.2800830152838844622 ) ) ;
#18381=CARTESIAN_POINT ( 'NONE',  ( 3.999999999999998224, 2.472263674411418588, -3.687027874309861897 ) ) ;
#18394=AXIS2_PLACEMENT_3D ( 'NONE', #7610, #389, #9694 ) ;
#18419=EDGE_CURVE ( 'NONE', #13534, #13337, #20370, .T. ) ;
#18436=DIRECTION ( 'NONE',  ( -0.000000000000000000, -0.000000000000000000, 1.000000000000000000 ) ) ;
#18443=CARTESIAN_POINT ( 'NONE',  ( 4.000000000000000000, 2.309401076758497151, -3.433295621305379353 ) ) ;
#18445=CARTESIAN_POINT ( 'NONE',  ( 4.000000000000000000, 0.000000000000000000, 0.000000000000000000 ) ) ;
#18514=CARTESIAN_POINT ( 'NONE',  ( 0.3461262719736147297, -4.658553426539303821, -3.671615880910379381 ) ) ;
#18548=CARTESIAN_POINT ( 'NONE',  ( -6.259644161404860030E-16, -4.618802153517027165, -5.000000000000000000 ) ) ;
#18554=CARTESIAN_POINT ( 'NONE',  ( -4.000000000000000000, 0.9868501483902560878, -0.09357334158579519445 ) ) ;
#18570=DIRECTION ( 'NONE',  ( -0.000000000000000000, -0.000000000000000000, 1.000000000000000000 ) ) ;
#18607=AXIS2_PLACEMENT_3D ( 'NONE', #2729, #4663, #17565 ) ;
#18611=CARTESIAN_POINT ( 'NONE',  ( 1.411581201560190495E-15, 4.862606272033091592, -3.745885042887436622 ) ) ;
#18658=CARTESIAN_POINT ( 'NONE',  ( -2.344047193898593395, -3.265465875126480455, -1.054683074273691752E-14 ) ) ;
#18665=CARTESIAN_POINT ( 'NONE',  ( -3.264650091097280831E-13, -4.796980096169642493, -3.721999068284424617 ) ) ;
#18670=EDGE_CURVE ( 'NONE', #20231, #16162, #19214, .T. ) ;
#18678=ORIENTED_EDGE ( 'NONE', *, *, #1831, .T. ) ;
#18685=AXIS2_PLACEMENT_3D ( 'NONE', #21357, #19531, #6634 ) ;
#18704=CARTESIAN_POINT ( 'NONE',  ( 4.000000000000000000, -2.309401076758516691, -0.4999999999999995559 ) ) ;
#18714=EDGE_CURVE ( 'NONE', #1398, #14870, #611, .T. ) ;
#18745=EDGE_CURVE ( 'NONE', #21528, #9606, #13247, .T. ) ;
#18781=EDGE_CURVE ( 'NONE', #14870, #1398, #15280, .T. ) ;
#18831=( BOUNDED_SURFACE ( )  B_SPLINE_SURFACE ( 3, 2, ( 
 ( #7410, #5478, #8994 ),
 ( #2078, #14791, #9469 ),
 ( #20090, #3643, #1836 ),
 ( #3766, #23595, #13129 ),
 ( #11059, #22119, #1613 ),
 ( #23702, #18381, #9110 ) ),
 .UNSPECIFIED., .F., .F., .F. ) 
 B_SPLINE_SURFACE_WITH_KNOTS ( ( 4, 2, 4 ),
 ( 3, 3 ),
 ( 0.02027065861071770947, 0.02273072267836921331, 0.02519078674602071716 ),
 ( 0.000000000000000000, 1.000000000000000000 ),
 .UNSPECIFIED. ) 
 GEOMETRIC_REPRESENTATION_ITEM ( )  RATIONAL_B_SPLINE_SURFACE ( (
 ( 1.000000000000000000, 0.8047781708337304885, 1.000000000000000000),
 ( 1.000000000000000000, 0.8123765190705307671, 1.000000000000000000),
 ( 1.000000000000000000, 0.8190656277163975707, 1.000000000000000000),
 ( 1.000000000000000000, 0.8192366903512159348, 1.000000000000000000),
 ( 1.000000000000000000, 0.8126138454302893610, 1.000000000000000000),
 ( 1.000000000000000000, 0.8047712246031417660, 1.000000000000000000) ) ) 
 REPRESENTATION_ITEM ( '' )  SURFACE ( )  );
#18876=CARTESIAN_POINT ( 'NONE',  ( -4.000000000000000000, 2.309401076758498483, -3.433295621305379353 ) ) ;
#18907=FACE_OUTER_BOUND ( 'NONE', #19322, .T. ) ;
#18947=CARTESIAN_POINT ( 'NONE',  ( 1.654252653721905331, 3.663718938583014229, -0.01223254789873410957 ) ) ;
#18972=CARTESIAN_POINT ( 'NONE',  ( 4.211140560182196957, 2.431303136016536470, -3.745885042887433514 ) ) ;
#18980=ORIENTED_EDGE ( 'NONE', *, *, #14744, .F. ) ;
#18987=CARTESIAN_POINT ( 'NONE',  ( 0.000000000000000000, 0.000000000000000000, 0.000000000000000000 ) ) ;
#19023=ADVANCED_FACE ( 'NONE', ( #6693 ), #8383, .F. ) ;
#19030=ORIENTED_EDGE ( 'NONE', *, *, #18781, .T. ) ;
#19076=CARTESIAN_POINT ( 'NONE',  ( 3.861362476283255685, 2.629030857715988656, -3.671615880910370500 ) ) ;
#19115=CARTESIAN_POINT ( 'NONE',  ( -1.999999999999999556, 3.464101615137754830, -3.142992957459232795 ) ) ;
#19168=FACE_OUTER_BOUND ( 'NONE', #10481, .T. ) ;
#19172=EDGE_LOOP ( 'NONE', ( #17553, #21162, #21534, #3721 ) ) ;
#19178=AXIS2_PLACEMENT_3D ( 'NONE', #7104, #18436, #10759 ) ;
#19185=CARTESIAN_POINT ( 'NONE',  ( 1.390230914382191596, 4.043987460488659202, -3.502507215260488582 ) ) ;
#19192=CARTESIAN_POINT ( 'NONE',  ( -4.197393957002303999, -0.8151795401431414234, -3.503767560748935139 ) ) ;
#19195=ADVANCED_FACE ( 'NONE', ( #608 ), #6368, .F. ) ;
#19205=VECTOR ( 'NONE', #14248, 1000.000000000000227 ) ;
#19214=B_SPLINE_CURVE_WITH_KNOTS ( 'NONE', 3,
 ( #1631, #7316, #10862, #14702, #3198 ),
 .UNSPECIFIED., .F., .F.,
 ( 4, 1, 4 ),
 ( 0.000000000000000000, 0.002309401076758505790, 0.004618802153517011580 ),
 .UNSPECIFIED. ) ;
#19222=EDGE_CURVE ( 'NONE', #12526, #13534, #4817, .T. ) ;
#19253=CIRCLE ( 'NONE', #11992, 5.560781378645573980 ) ;
#19274=LINE ( 'NONE', #23005, #11709 ) ;
#19307=CARTESIAN_POINT ( 'NONE',  ( -4.101948962585905356, -2.368261337751088824, -3.681124513963624167 ) ) ;
#19311=CARTESIAN_POINT ( 'NONE',  ( 1.287237434362044075, 3.875615274277557809, -3.430618716626812059 ) ) ;
#19313=CARTESIAN_POINT ( 'NONE',  ( 4.175648173966055587, -2.207990556236547608, -3.469390959564065291 ) ) ;
#19322=EDGE_LOOP ( 'NONE', ( #22821, #13365, #5355, #10290, #23536 ) ) ;
#19372=DIRECTION ( 'NONE',  ( -0.000000000000000000, 0.000000000000000000, -1.000000000000000000 ) ) ;
#19400=ORIENTED_EDGE ( 'NONE', *, *, #22250, .T. ) ;
#19449=ADVANCED_FACE ( 'NONE', ( #11005 ), #15443, .T. ) ;
#19495=CARTESIAN_POINT ( 'NONE',  ( -4.000000000000000000, -2.309401076758512694, -3.433295621305382461 ) ) ;
#19531=DIRECTION ( 'NONE',  ( 0.000000000000000000, -1.000000000000000000, 0.000000000000000000 ) ) ;
#19536=DIRECTION ( 'NONE',  ( -0.000000000000000000, -0.000000000000000000, 1.000000000000000000 ) ) ;
#19561=CARTESIAN_POINT ( 'NONE',  ( -0.3208286057739654917, 4.433571671609680465, -0.3503314178412548774 ) ) ;
#19565=AXIS2_PLACEMENT_3D ( 'NONE', #20419, #3880, #5825 ) ;
#19574=CARTESIAN_POINT ( 'NONE',  ( 4.000000000000000000, 0.3987449864460005378, -0.01220643443059817035 ) ) ;
#19575=AXIS2_PLACEMENT_3D ( 'NONE', #1726, #10952, #5483 ) ;
#19611=CARTESIAN_POINT ( 'NONE',  ( -4.000000000000000000, -0.8382240730041925492, -3.220610619767135141 ) ) ;
#19632=ORIENTED_EDGE ( 'NONE', *, *, #21867, .F. ) ;
#19642=LINE ( 'NONE', #3329, #2630 ) ;
#19652=AXIS2_PLACEMENT_3D ( 'NONE', #3779, #21788, #5254 ) ;
#19664=ORIENTED_EDGE ( 'NONE', *, *, #3097, .T. ) ;
#19679=EDGE_CURVE ( 'NONE', #9606, #5897, #16454, .T. ) ;
#19698=APPLICATION_CONTEXT ( 'automotive_design' ) ;
#19717=CARTESIAN_POINT ( 'NONE',  ( -4.211140560182196957, -2.431303136016552013, -3.745885042887436178 ) ) ;
#19790=B_SPLINE_CURVE_WITH_KNOTS ( 'NONE', 3,
 ( #11250, #222, #2131, #11353, #18665, #3831 ),
 .UNSPECIFIED., .F., .F.,
 ( 4, 2, 4 ),
 ( 0.000000000000000000, 0.0002095117440854740156, 0.0004190234881709480313 ),
 .UNSPECIFIED. ) ;
#19794=EDGE_LOOP ( 'NONE', ( #20745, #14136, #890, #15978 ) ) ;
#19859=CARTESIAN_POINT ( 'NONE',  ( -1.360585162435467455, 4.061296242128285883, -3.505054077164959203 ) ) ;
#19861=CIRCLE ( 'NONE', #9463, 0.5155456020628804703 ) ;
#19887=DIRECTION ( 'NONE',  ( 0.000000000000000000, 0.000000000000000000, -1.000000000000000000 ) ) ;
#19904=CARTESIAN_POINT ( 'NONE',  ( -4.024497503033519941, 2.323544716729375459, -3.572167766733379768 ) ) ;
#19911=AXIS2_PLACEMENT_3D ( 'NONE', #15161, #293, #2338 ) ;
#19930=CARTESIAN_POINT ( 'NONE',  ( 1.734723475976807094E-15, 4.618802153517012954, -0.4999999999999995559 ) ) ;
#19945=ORIENTED_EDGE ( 'NONE', *, *, #4335, .F. ) ;
#19949=VERTEX_POINT ( 'NONE', #7914 ) ;
#19957=CYLINDRICAL_SURFACE ( 'NONE', #7155, 2.100000000000000089 ) ;
#19961=CARTESIAN_POINT ( 'NONE',  ( 0.6937372685066666156, -4.453844082567737672, -3.610536846335894445 ) ) ;
#19968=AXIS2_PLACEMENT_3D ( 'NONE', #20121, #7086, #14474 ) ;
#19973=AXIS2_PLACEMENT_3D ( 'NONE', #5019, #10705, #17812 ) ;
#20008=CONICAL_SURFACE ( 'NONE', #7288, 4.000000000000000000, 0.8911886515913786111 ) ;
#20052=ORIENTED_EDGE ( 'NONE', *, *, #21109, .T. ) ;
#20063=PRODUCT_DEFINITION_FORMATION_WITH_SPECIFIED_SOURCE ( 'ANY', '', #13866, .NOT_KNOWN. ) ;
#20081=CARTESIAN_POINT ( 'NONE',  ( 2.290893957444128645E-15, 4.647089433458768681, -3.572167766733382877 ) ) ;
#20090=CARTESIAN_POINT ( 'NONE',  ( 4.000000000000000000, -0.8732470631449981147, -3.223155494240760088 ) ) ;
#20094=ORIENTED_EDGE ( 'NONE', *, *, #14191, .F. ) ;
#20115=DIRECTION ( 'NONE',  ( 1.000000000000000000, 0.000000000000000000, 0.000000000000000000 ) ) ;
#20117=CARTESIAN_POINT ( 'NONE',  ( 4.154306624731137099, 2.398490048084935822, -3.721999068284414847 ) ) ;
#20121=CARTESIAN_POINT ( 'NONE',  ( 0.000000000000000000, 0.000000000000000000, -5.000000000000000000 ) ) ;
#20146=CARTESIAN_POINT ( 'NONE',  ( 1.567478505476134606E-15, 4.618802153517012066, -3.433295621305382905 ) ) ;
#20158=CARTESIAN_POINT ( 'NONE',  ( 2.500000000000000888, 3.061616997868384127E-16, -4.974599999999998801 ) ) ;
#20161=CARTESIAN_POINT ( 'NONE',  ( 1.312671235360372224, 3.860931062424219462, -0.05923475698270440348 ) ) ;
#20173=CARTESIAN_POINT ( 'NONE',  ( 0.000000000000000000, 0.000000000000000000, 3.469446951953614189E-15 ) ) ;
#20174=CARTESIAN_POINT ( 'NONE',  ( 3.999999999999999112, 1.941961291383486277, -0.3515519931180248192 ) ) ;
#20190=EDGE_CURVE ( 'NONE', #5401, #9508, #287, .T. ) ;
#20203=CARTESIAN_POINT ( 'NONE',  ( -0.5469614295416921346, 4.303013824936271270, -3.535263753543735454 ) ) ;
#20216=DIRECTION ( 'NONE',  ( -0.000000000000000000, -0.000000000000000000, 1.000000000000000000 ) ) ;
#20231=VERTEX_POINT ( 'NONE', #17185 ) ;
#20245=DIRECTION ( 'NONE',  ( 1.224646799147353207E-16, 1.000000000000000000, 0.000000000000000000 ) ) ;
#20264=UNCERTAINTY_MEASURE_WITH_UNIT (LENGTH_MEASURE( 1.000000000000000082E-05 ), #18227, 'distance_accuracy_value', 'NONE');
#20370=B_SPLINE_CURVE_WITH_KNOTS ( 'NONE', 3,
 ( #7942, #22535, #11843, #15204, #20601, #11721 ),
 .UNSPECIFIED., .F., .F.,
 ( 4, 2, 4 ),
 ( 0.002452478801916361129, 0.003676905084148001344, 0.004901331366379641126 ),
 .UNSPECIFIED. ) ;
#20373=CARTESIAN_POINT ( 'NONE',  ( 4.000000000000000000, 2.309401076758497151, -3.433295621305379353 ) ) ;
#20384=CARTESIAN_POINT ( 'NONE',  ( 2.000000000000008882, 3.464101615137749945, 0.000000000000000000 ) ) ;
#20393=COLOUR_RGB ( '',1.000000000000000000, 0.9490196078431372140, 0.9098039215686274384 ) ;
#20419=CARTESIAN_POINT ( 'NONE',  ( 0.000000000000000000, 0.000000000000000000, -0.3080913168122742518 ) ) ;
#20435=FACE_OUTER_BOUND ( 'NONE', #19794, .T. ) ;
#20443=FACE_OUTER_BOUND ( 'NONE', #6720, .T. ) ;
#20473=CARTESIAN_POINT ( 'NONE',  ( -4.000000000000000000, -1.560351142792950618, -0.2242961665059814425 ) ) ;
#20479=CARTESIAN_POINT ( 'NONE',  ( -2.100000000000000089, 2.571758278209441957E-16, -4.694516984716113228 ) ) ;
#20495=DIRECTION ( 'NONE',  ( 0.000000000000000000, 0.000000000000000000, -1.000000000000000000 ) ) ;
#20500=CARTESIAN_POINT ( 'NONE',  ( 4.000000000000000000, 2.309401076758497151, -5.000000000000000000 ) ) ;
#20517=CARTESIAN_POINT ( 'NONE',  ( 2.000000000000008882, 3.464101615137749945, 0.000000000000000000 ) ) ;
#20540=ORIENTED_EDGE ( 'NONE', *, *, #1679, .T. ) ;
#20573=VECTOR ( 'NONE', #13272, 1000.000000000000000 ) ;
#20601=CARTESIAN_POINT ( 'NONE',  ( 4.207491450040567571, -2.029819825146485179, -3.671670828759567407 ) ) ;
#20604=ORIENTED_EDGE ( 'NONE', *, *, #21867, .T. ) ;
#20668=EDGE_CURVE ( 'NONE', #21528, #1506, #19642, .T. ) ;
#20670=CARTESIAN_POINT ( 'NONE',  ( -0.6937372685066653943, 4.453844082567723461, -3.610536846335889116 ) ) ;
#20672=DIRECTION ( 'NONE',  ( -1.000000000000000000, 0.000000000000000000, 0.000000000000000000 ) ) ;
#20683=ORIENTED_EDGE ( 'NONE', *, *, #5095, .F. ) ;
#20695=EDGE_CURVE ( 'NONE', #10625, #20887, #23153, .T. ) ;
#20697=ORIENTED_EDGE ( 'NONE', *, *, #13037, .T. ) ;
#20705=DIRECTION ( 'NONE',  ( -1.000000000000000000, 0.000000000000000000, 0.000000000000000000 ) ) ;
#20730=VECTOR ( 'NONE', #15180, 1000.000000000000000 ) ;
#20740=DIRECTION ( 'NONE',  ( 0.000000000000000000, 0.000000000000000000, -1.000000000000000000 ) ) ;
#20745=ORIENTED_EDGE ( 'NONE', *, *, #13037, .F. ) ;
#20754=ORIENTED_EDGE ( 'NONE', *, *, #9762, .T. ) ;
#20756=CARTESIAN_POINT ( 'NONE',  ( 0.5636800770130377947, 4.293361309317166530, -3.531542292954102713 ) ) ;
#20792=( LENGTH_UNIT ( ) NAMED_UNIT ( * ) SI_UNIT ( .MILLI., .METRE. ) );
#20810=AXIS2_PLACEMENT_3D ( 'NONE', #21796, #10360, #8778 ) ;
#20827=AXIS2_PLACEMENT_3D ( 'NONE', #20173, #18023, #5339 ) ;
#20829=AXIS2_PLACEMENT_3D ( 'NONE', #13558, #17251, #696 ) ;
#20844=CARTESIAN_POINT ( 'NONE',  ( -6.473970235329672780E-16, -4.862606272033106691, -3.745885042887442395 ) ) ;
#20875=UNCERTAINTY_MEASURE_WITH_UNIT (LENGTH_MEASURE( 1.000000000000000082E-05 ), #20792, 'distance_accuracy_value', 'NONE');
#20878=ORIENTED_EDGE ( 'NONE', *, *, #9187, .T. ) ;
#20887=VERTEX_POINT ( 'NONE', #11089 ) ;
#20897=FACE_OUTER_BOUND ( 'NONE', #22947, .T. ) ;
#20910=CARTESIAN_POINT ( 'NONE',  ( 1.567478505476134606E-15, 4.618802153517012066, -3.433295621305382905 ) ) ;
#20926=DIRECTION ( 'NONE',  ( -0.000000000000000000, 0.000000000000000000, -1.000000000000000000 ) ) ;
#20943=DIRECTION ( 'NONE',  ( 1.000000000000000000, 0.000000000000000000, 0.000000000000000000 ) ) ;
#20950=CARTESIAN_POINT ( 'NONE',  ( -0.3198814748697807464, -4.434118497892185040, -0.3507732604232532969 ) ) ;
#20960=( LENGTH_UNIT ( ) NAMED_UNIT ( * ) SI_UNIT ( .MILLI., .METRE. ) );
#21005=CARTESIAN_POINT ( 'NONE',  ( -4.000000000000000888, -2.309401076758512694, -3.504269196027526512 ) ) ;
#21009=CARTESIAN_POINT ( 'NONE',  ( 4.197393957002303999, 0.8151795401431359833, -3.503767560748935139 ) ) ;
#21078=DIRECTION ( 'NONE',  ( -1.000000000000000000, 0.000000000000000000, 0.000000000000000000 ) ) ;
#21079=CARTESIAN_POINT ( 'NONE',  ( -4.000000000000000000, -2.512220745329312610, -3.469390707569719901 ) ) ;
#21090=CARTESIAN_POINT ( 'NONE',  ( -3.680118525130244400, 2.494084732383327285, -0.3507732604232449702 ) ) ;
#21109=EDGE_CURVE ( 'NONE', #21209, #18124, #21911, .T. ) ;
#21118=EDGE_LOOP ( 'NONE', ( #10628, #13486, #12496, #22813, #6192 ) ) ;
#21129=CARTESIAN_POINT ( 'NONE',  ( 3.436319922986518449, -2.634841920959471562, -3.531542292954761741 ) ) ;
#21162=ORIENTED_EDGE ( 'NONE', *, *, #5095, .T. ) ;
#21204=ORIENTED_EDGE ( 'NONE', *, *, #18745, .T. ) ;
#21206=CARTESIAN_POINT ( 'NONE',  ( -4.204114297095464359, 1.660363174096617156, -3.602136431857887011 ) ) ;
#21209=VERTEX_POINT ( 'NONE', #10113 ) ;
#21229=CARTESIAN_POINT ( 'NONE',  ( 4.000000000000000000, 2.309401076758497151, -3.433295621305379353 ) ) ;
#21260=CARTESIAN_POINT ( 'NONE',  ( 0.5276280594147412240, -4.314175951381924889, -3.320322319201654881 ) ) ;
#21278=EDGE_LOOP ( 'NONE', ( #17194, #14516, #16294, #2553 ) ) ;
#21304=CARTESIAN_POINT ( 'NONE',  ( 0.1410422978106145031, -4.700232962125109104, -3.687027686973628704 ) ) ;
#21312=EDGE_CURVE ( 'NONE', #10625, #5401, #3450, .T. ) ;
#21322=( BOUNDED_SURFACE ( )  B_SPLINE_SURFACE ( 3, 2, ( 
 ( #13935, #22926, #6759 ),
 ( #21260, #14156, #953 ),
 ( #1072, #14039, #8459 ),
 ( #4709, #15949, #13807 ),
 ( #23179, #21129, #12012 ),
 ( #19313, #6645, #8332 ) ),
 .UNSPECIFIED., .F., .F., .F. ) 
 B_SPLINE_SURFACE_WITH_KNOTS ( ( 4, 2, 4 ),
 ( 3, 3 ),
 ( 0.02032853247518126918, 0.02278863295364821906, 0.02524873343211517240 ),
 ( 0.000000000000000000, 1.000000000000000000 ),
 .UNSPECIFIED. ) 
 GEOMETRIC_REPRESENTATION_ITEM ( )  RATIONAL_B_SPLINE_SURFACE ( (
 ( 1.000000000000000000, 0.8047781615896837382, 1.000000000000000000),
 ( 1.000000000000000000, 0.8123767586289252218, 1.000000000000000000),
 ( 1.000000000000000000, 0.8190662415564388121, 1.000000000000000000),
 ( 1.000000000000000000, 0.8192361015669026303, 1.000000000000000000),
 ( 1.000000000000000000, 0.8126135807103900266, 1.000000000000000000),
 ( 1.000000000000000000, 0.8047712338318593339, 1.000000000000000000) ) ) 
 REPRESENTATION_ITEM ( '' )  SURFACE ( )  );
#21357=CARTESIAN_POINT ( 'NONE',  ( 5.384454397937118664, 0.000000000000000000, -4.484454397937119197 ) ) ;
#21366=AXIS2_PLACEMENT_3D ( 'NONE', #12814, #3561, #20115 ) ;
#21405=AXIS2_PLACEMENT_3D ( 'NONE', #4451, #22673, #4334 ) ;
#21430=CARTESIAN_POINT ( 'NONE',  ( 0.000000000000000000, 0.000000000000000000, -4.974599999999998801 ) ) ;
#21431=CARTESIAN_POINT ( 'NONE',  ( -4.000000000000000000, -0.8232339106130515116, -3.430630286862743183 ) ) ;
#21443=CARTESIAN_POINT ( 'NONE',  ( 4.024499207728657879, -2.323545700935587988, -3.572172305156509964 ) ) ;
#21453=CARTESIAN_POINT ( 'NONE',  ( 4.000000000000000888, 1.539600717838996990, -3.300726591567079815 ) ) ;
#21468=CARTESIAN_POINT ( 'NONE',  ( 2.804994570502171047, 3.229033611042449792, -3.526374918436834704 ) ) ;
#21528=VERTEX_POINT ( 'NONE', #6788 ) ;
#21534=ORIENTED_EDGE ( 'NONE', *, *, #6055, .T. ) ;
#21543=PLANE ( 'NONE',  #19973 ) ;
#21616=AXIS2_PLACEMENT_3D ( 'NONE', #18548, #18308, #1547 ) ;
#21723=ADVANCED_FACE ( 'NONE', ( #2300 ), #9950, .F. ) ;
#21725=ORIENTED_EDGE ( 'NONE', *, *, #1679, .F. ) ;
#21731=CARTESIAN_POINT ( 'NONE',  ( 3.999999999999999112, -0.3979232138631231819, -5.929230630780099908E-17 ) ) ;
#21751=DIRECTION ( 'NONE',  ( -0.000000000000000000, -0.000000000000000000, 1.000000000000000000 ) ) ;
#21774=ORIENTED_EDGE ( 'NONE', *, *, #11892, .T. ) ;
#21783=ORIENTED_EDGE ( 'NONE', *, *, #4305, .F. ) ;
#21785=CARTESIAN_POINT ( 'NONE',  ( -4.236525694536558362, 2.416953475386465211, -3.751298745799836354 ) ) ;
#21788=DIRECTION ( 'NONE',  ( 0.000000000000000000, -0.000000000000000000, 1.000000000000000000 ) ) ;
#21796=CARTESIAN_POINT ( 'NONE',  ( 0.000000000000000000, 0.000000000000000000, -5.000000000000000000 ) ) ;
#21841=( NAMED_UNIT ( * ) PLANE_ANGLE_UNIT ( ) SI_UNIT ( $, .RADIAN. ) );
#21851=CARTESIAN_POINT ( 'NONE',  ( 4.000000000000000000, -2.309401076758514915, -5.000000000000000000 ) ) ;
#21860=VERTEX_POINT ( 'NONE', #3829 ) ;
#21867=EDGE_CURVE ( 'NONE', #1352, #160, #1048, .T. ) ;
#21898=ORIENTED_EDGE ( 'NONE', *, *, #10672, .F. ) ;
#21911=CIRCLE ( 'NONE', #4182, 4.000000000000000000 ) ;
#21920=CARTESIAN_POINT ( 'NONE',  ( -4.000000000000000000, -2.309401076758515803, -0.4999999999999995559 ) ) ;
#21960=CIRCLE ( 'NONE', #12369, 4.000000000000000000 ) ;
#21961=CARTESIAN_POINT ( 'NONE',  ( -2.059999999999998721, 2.522772406243545965E-16, -0.3080913168122742518 ) ) ;
#21966=DIRECTION ( 'NONE',  ( 1.000000000000000000, 0.000000000000000000, 0.000000000000000000 ) ) ;
#21983=CARTESIAN_POINT ( 'NONE',  ( -2.836893136758495970, -3.208949435745868328, -3.505054077164885484 ) ) ;
#21986=CARTESIAN_POINT ( 'NONE',  ( 1.144235203016666258, 3.958177651039090250, -0.09382832055445661235 ) ) ;
#22009=DIRECTION ( 'NONE',  ( 1.000000000000000000, 0.000000000000000000, 0.000000000000000000 ) ) ;
#22013=DIRECTION ( 'NONE',  ( 1.000000000000000000, 0.000000000000000000, 0.000000000000000000 ) ) ;
#22020=B_SPLINE_CURVE_WITH_KNOTS ( 'NONE', 3,
 ( #16853, #3678, #9271, #11227, #20117, #316 ),
 .UNSPECIFIED., .F., .F.,
 ( 4, 2, 4 ),
 ( 0.000000000000000000, 0.0002095117440854730670, 0.0004190234881709461339 ),
 .UNSPECIFIED. ) ;
#22039=CARTESIAN_POINT ( 'NONE',  ( -4.000000000000000000, -2.309401076758515803, -0.4999999999999995559 ) ) ;
#22048=ORIENTED_EDGE ( 'NONE', *, *, #14092, .T. ) ;
#22049=ORIENTED_EDGE ( 'NONE', *, *, #4335, .T. ) ;
#22068=DIRECTION ( 'NONE',  ( -1.000000000000000000, 0.000000000000000000, 0.000000000000000000 ) ) ;
#22119=CARTESIAN_POINT ( 'NONE',  ( 4.000000000001088907, 1.658577278524410170, -3.531553309554541720 ) ) ;
#22173=CARTESIAN_POINT ( 'NONE',  ( -5.384454397937118664, 6.594054843588581554E-16, -4.484454397937119197 ) ) ;
#22222=FACE_OUTER_BOUND ( 'NONE', #8804, .T. ) ;
#22233=AXIS2_PLACEMENT_3D ( 'NONE', #5796, #18570, #21966 ) ;
#22250=EDGE_CURVE ( 'NONE', #1506, #23662, #8526, .T. ) ;
#22291=CARTESIAN_POINT ( 'NONE',  ( -3.349226789952655547, -2.685125164760744809, -0.2236248678334863682 ) ) ;
#22306=EDGE_CURVE ( 'NONE', #1398, #17675, #15427, .T. ) ;
#22327=MECHANICAL_DESIGN_GEOMETRIC_PRESENTATION_REPRESENTATION('',(#15789),#7690);
#22400=ADVANCED_FACE ( 'NONE', ( #23230 ), #21543, .T. ) ;
#22402=CARTESIAN_POINT ( 'NONE',  ( 2.344047193898588954, 3.265465875126468021, -5.031375706690542042E-16 ) ) ;
#22449=CARTESIAN_POINT ( 'NONE',  ( 1.734723475976807094E-15, 4.618802153517012954, -0.4999999999999995559 ) ) ;
#22471=EDGE_LOOP ( 'NONE', ( #13967, #9541, #11201, #8914 ) ) ;
#22512=CARTESIAN_POINT ( 'NONE',  ( -1.144235203016679359, -3.958177651039096911, -0.09382832055446428676 ) ) ;
#22535=CARTESIAN_POINT ( 'NONE',  ( 4.197393957002303999, -0.4069871074557456780, -3.503767560748925813 ) ) ;
#22562=ADVANCED_FACE ( 'NONE', ( #20443 ), #18831, .F. ) ;
#22566=CARTESIAN_POINT ( 'NONE',  ( -0.1756481739660520902, 4.720212674038980261, -3.469390959564065291 ) ) ;
#22573=DIRECTION ( 'NONE',  ( 0.000000000000000000, 0.000000000000000000, 1.000000000000000000 ) ) ;
#22582=ORIENTED_EDGE ( 'NONE', *, *, #23430, .T. ) ;
#22597=EDGE_CURVE ( 'NONE', #13337, #13636, #7051, .T. ) ;
#22601=DIRECTION ( 'NONE',  ( 0.000000000000000000, 0.000000000000000000, 1.000000000000000000 ) ) ;
#22635=EDGE_CURVE ( 'NONE', #5897, #17167, #23181, .T. ) ;
#22669=ADVANCED_FACE ( 'NONE', ( #15269, #17619 ), #2327, .T. ) ;
#22673=DIRECTION ( 'NONE',  ( -0.5000000000000019984, -0.8660254037844375974, 0.000000000000000000 ) ) ;
#22689=CARTESIAN_POINT ( 'NONE',  ( 3.453038570460273071, 2.625189405340834448, -3.535263753543585352 ) ) ;
#22700=DIRECTION ( 'NONE',  ( -1.000000000000000000, 0.000000000000000000, 0.000000000000000000 ) ) ;
#22739=CARTESIAN_POINT ( 'NONE',  ( 1.411581201560190495E-15, 4.862606272033091592, -3.745885042887436622 ) ) ;
#22813=ORIENTED_EDGE ( 'NONE', *, *, #5618, .T. ) ;
#22815=CARTESIAN_POINT ( 'NONE',  ( 3.472371940585993855, 2.614027278893175321, -3.320322319201766792 ) ) ;
#22821=ORIENTED_EDGE ( 'NONE', *, *, #4599, .T. ) ;
#22823=CARTESIAN_POINT ( 'NONE',  ( 1.391697335622810172, 4.043246145443375461, -3.503898532754365913 ) ) ;
#22872=DIRECTION ( 'NONE',  ( -0.000000000000000000, 0.000000000000000000, -1.000000000000000000 ) ) ;
#22912=EDGE_LOOP ( 'NONE', ( #19632, #7385, #564 ) ) ;
#22926=CARTESIAN_POINT ( 'NONE',  ( -0.1404048886732797152, -4.699864953788083888, -3.686887068327043160 ) ) ;
#22931=CARTESIAN_POINT ( 'NONE',  ( -4.197393957002303999, -7.773935952363655451E-14, -3.503767560748929810 ) ) ;
#22947=EDGE_LOOP ( 'NONE', ( #6925, #3940, #2368, #6885, #4568 ) ) ;
#22949=CARTESIAN_POINT ( 'NONE',  ( -2.000000000000006661, 3.464101615137750834, 0.000000000000000000 ) ) ;
#22983=CARTESIAN_POINT ( 'NONE',  ( -2.000000000000007550, -3.464101615137749945, 0.000000000000000000 ) ) ;
#22986=CARTESIAN_POINT ( 'NONE',  ( -2.449848172108560540, -3.432307619358754724, -3.503702292528910078 ) ) ;
#23004=CARTESIAN_POINT ( 'NONE',  ( 4.000000000000000000, -2.309401076758514915, -3.433295621305383349 ) ) ;
#23005=CARTESIAN_POINT ( 'NONE',  ( -4.000000000000000000, 2.309401076758498483, -5.000000000000000000 ) ) ;
#23009=B_SPLINE_CURVE_WITH_KNOTS ( 'NONE', 3,
 ( #15132, #7861, #19192, #22931 ),
 .UNSPECIFIED., .F., .F.,
 ( 4, 4 ),
 ( 0.000000000000000000, 0.002452478801916376308 ),
 .UNSPECIFIED. ) ;
#23032=ORIENTED_EDGE ( 'NONE', *, *, #8852, .F. ) ;
#23034=CIRCLE ( 'NONE', #18034, 2.500000000000000444 ) ;
#23047=CARTESIAN_POINT ( 'NONE',  ( 8.673617379884035472E-16, 4.618802153517012954, -5.000000000000000000 ) ) ;
#23074=CARTESIAN_POINT ( 'NONE',  ( -4.211140560182196957, 2.431303136016537803, -3.745885042887433514 ) ) ;
#23103=CARTESIAN_POINT ( 'NONE',  ( -2.742827927723112236, -3.035229711105190464, -3.433252694550595230 ) ) ;
#23153=LINE ( 'NONE', #3105, #19205 ) ;
#23172=CYLINDRICAL_SURFACE ( 'NONE', #15196, 2.500000000000000444 ) ;
#23179=CARTESIAN_POINT ( 'NONE',  ( 3.455068668934414777, -2.624017327439094327, -3.316620875263732504 ) ) ;
#23181=LINE ( 'NONE', #13246, #3006 ) ;
#23230=FACE_OUTER_BOUND ( 'NONE', #2584, .T. ) ;
#23262=CARTESIAN_POINT ( 'NONE',  ( 0.000000000000000000, 0.000000000000000000, 0.000000000000000000 ) ) ;
#23363=CARTESIAN_POINT ( 'NONE',  ( -4.211405944401398038, -2.460460786169389902, -3.751298493805494072 ) ) ;
#23364=ORIENTED_EDGE ( 'NONE', *, *, #23478, .F. ) ;
#23423=ORIENTED_EDGE ( 'NONE', *, *, #22635, .T. ) ;
#23430=EDGE_CURVE ( 'NONE', #5897, #12526, #22020, .T. ) ;
#23478=EDGE_CURVE ( 'NONE', #12107, #21209, #7598, .T. ) ;
#23527=AXIS2_PLACEMENT_3D ( 'NONE', #5407, #19887, #7442 ) ;
#23536=ORIENTED_EDGE ( 'NONE', *, *, #8240, .F. ) ;
#23554=( NAMED_UNIT ( * ) SI_UNIT ( $, .STERADIAN. ) SOLID_ANGLE_UNIT ( ) );
#23595=CARTESIAN_POINT ( 'NONE',  ( 4.000000000000000888, 0.8228435280416209752, -3.430609588141487976 ) ) ;
#23601=CARTESIAN_POINT ( 'NONE',  ( -3.455068668934486276, 2.624017327439035707, -3.316620875263955437 ) ) ;
#23622=DIRECTION ( 'NONE',  ( -0.000000000000000000, -0.000000000000000000, 1.000000000000000000 ) ) ;
#23630=CYLINDRICAL_SURFACE ( 'NONE', #19968, 2.100000000000000089 ) ;
#23640=EDGE_CURVE ( 'NONE', #13636, #3749, #16802, .T. ) ;
#23662=VERTEX_POINT ( 'NONE', #6108 ) ;
#23702=CARTESIAN_POINT ( 'NONE',  ( 4.000000000000000000, 2.512223110932545023, -3.469391141908803711 ) ) ;
#23721=ORIENTED_EDGE ( 'NONE', *, *, #3975, .F. ) ;
#23761=CARTESIAN_POINT ( 'NONE',  ( 0.000000000000000000, 0.000000000000000000, -4.000000000000000000 ) ) ;
#23766=CARTESIAN_POINT ( 'NONE',  ( 4.000000000000000000, -2.309401076758516691, -0.4999999999999995559 ) ) ;
#23786=CARTESIAN_POINT ( 'NONE',  ( 0.6448876103708359731, 4.246476118072354922, -0.2256878752776725616 ) ) ;
#23799=DIRECTION ( 'NONE',  ( -0.8191520442889902442, 0.000000000000000000, -0.5735764363510482688 ) ) ;
#23800=CARTESIAN_POINT ( 'NONE',  ( 4.000000000000000000, 0.9868501483902631932, -0.09357334158579604100 ) ) ;
#23921=COLOUR_RGB('Black',0.12,0.14,0.17);
#23922=FILL_AREA_STYLE_COLOUR('',#23921);
#23923=FILL_AREA_STYLE('',(#23922));
#23924=SURFACE_STYLE_FILL_AREA(#23923);
#23925=SURFACE_SIDE_STYLE('',(#23924));
#23926=SURFACE_STYLE_USAGE(.BOTH.,#23925);
#23927=PRESENTATION_STYLE_ASSIGNMENT((#23926));
ENDSEC;
END-ISO-10303-21;
